ISO-10303-21;
HEADER;
FILE_DESCRIPTION (('STEP AP214'),
    '1' );
FILE_NAME ('8. Upper Jaw Support.step',
    '2026-10-09T08:13:37',
    ( '' ),
    ( '' ),
    'SwSTEP 2.0',
    'SolidWorks 2021',
    '' );
FILE_SCHEMA (( 'AUTOMOTIVE_DESIGN' ));
ENDSEC;

DATA;
#1=B_SPLINE_CURVE_WITH_KNOTS ( 'NONE', 3,
 ( #31451, #51902, #15336, #30765, #9698, #42087, #68086, #42425 ),
 .UNSPECIFIED., .F., .F.,
 ( 4, 2, 2, 4 ),
 ( 0.000000000000000000, 0.001617176559457151079, 0.002425764839185726510, 0.003234353118914302157 ),
 .UNSPECIFIED. ) ;
#16=PLANE ( 'NONE',  #47135 ) ;
#40=CARTESIAN_POINT ( 'NONE',  ( -47.09426399558999776, -13.61002330776443969, 0.8661849162379273714 ) ) ;
#44=AXIS2_PLACEMENT_3D ( 'NONE', #13603, #53264, #52575 ) ;
#51=CYLINDRICAL_SURFACE ( 'NONE', #37197, 1.000000000000000888 ) ;
#54=EDGE_LOOP ( 'NONE', ( #66784, #37211, #64174, #16099 ) ) ;
#77=EDGE_LOOP ( 'NONE', ( #67985, #68623, #51580, #57239 ) ) ;
#108=EDGE_CURVE ( 'NONE', #11830, #36200, #38610, .T. ) ;
#127=DIRECTION ( 'NONE',  ( -1.189524669241239115E-16, -1.000000000000000000, -0.000000000000000000 ) ) ;
#134=VECTOR ( 'NONE', #49583, 1000.000000000000000 ) ;
#139=DIRECTION ( 'NONE',  ( -1.000000000000000000, 0.000000000000000000, 0.000000000000000000 ) ) ;
#151=DIRECTION ( 'NONE',  ( -1.000000000000000000, 0.000000000000000000, 0.000000000000000000 ) ) ;
#158=AXIS2_PLACEMENT_3D ( 'NONE', #18232, #49917, #34060 ) ;
#175=ADVANCED_BREP_SHAPE_REPRESENTATION ( '', ( #4071, #42840 ), #64177 ) ;
#221=CARTESIAN_POINT ( 'NONE',  ( -71.75000000000000000, -3.000000000000000000, 19.00000000000000000 ) ) ;
#224=DIRECTION ( 'NONE',  ( -0.000000000000000000, 0.000000000000000000, -1.000000000000000000 ) ) ;
#230=DIRECTION ( 'NONE',  ( 1.000000000000000000, -1.189524669241239115E-16, -0.000000000000000000 ) ) ;
#231=AXIS2_PLACEMENT_3D ( 'NONE', #66179, #33824, #22947 ) ;
#282=ORIENTED_EDGE ( 'NONE', *, *, #38883, .T. ) ;
#294=ORIENTED_EDGE ( 'NONE', *, *, #44539, .F. ) ;
#298=DIRECTION ( 'NONE',  ( 0.000000000000000000, 0.000000000000000000, 1.000000000000000000 ) ) ;
#318=CARTESIAN_POINT ( 'NONE',  ( -75.75000000000000000, -0.9999999999999995559, 5.000000000000001776 ) ) ;
#322=CARTESIAN_POINT ( 'NONE',  ( -47.54356174116917089, -13.47739874223435486, 2.712348457220761677 ) ) ;
#323=CARTESIAN_POINT ( 'NONE',  ( -43.75000000000000000, 4.336808689942018722E-16, -5.099999999999999645 ) ) ;
#332=EDGE_CURVE ( 'NONE', #19277, #32327, #42649, .T. ) ;
#335=EDGE_LOOP ( 'NONE', ( #46322, #25808, #46956, #19729 ) ) ;
#354=EDGE_CURVE ( 'NONE', #25360, #68588, #1, .T. ) ;
#359=EDGE_CURVE ( 'NONE', #40324, #25898, #56986, .T. ) ;
#366=ORIENTED_EDGE ( 'NONE', *, *, #63470, .F. ) ;
#397=LINE ( 'NONE', #21925, #57054 ) ;
#399=AXIS2_PLACEMENT_3D ( 'NONE', #50431, #30330, #39914 ) ;
#424=DIRECTION ( 'NONE',  ( 1.000000000000000000, 0.000000000000000000, 0.000000000000000000 ) ) ;
#462=EDGE_CURVE ( 'NONE', #45832, #24916, #21603, .T. ) ;
#475=AXIS2_PLACEMENT_3D ( 'NONE', #59190, #10003, #26823 ) ;
#494=DIRECTION ( 'NONE',  ( -1.000000000000000000, 0.000000000000000000, 0.000000000000000000 ) ) ;
#497=CARTESIAN_POINT ( 'NONE',  ( 0.000000000000000000, -3.000000000000000000, 7.000000000000001776 ) ) ;
#545=ORIENTED_EDGE ( 'NONE', *, *, #1842, .F. ) ;
#563=VECTOR ( 'NONE', #25648, 1000.000000000000000 ) ;
#587=EDGE_CURVE ( 'NONE', #62302, #51825, #44499, .T. ) ;
#611=CARTESIAN_POINT ( 'NONE',  ( -53.60138881051016568, -9.947368421052628307, -2.000000000000000000 ) ) ;
#621=DIRECTION ( 'NONE',  ( 1.000000000000000000, 0.000000000000000000, 0.000000000000000000 ) ) ;
#651=EDGE_CURVE ( 'NONE', #30219, #13126, #54768, .T. ) ;
#653=DIRECTION ( 'NONE',  ( 0.000000000000000000, 0.000000000000000000, 1.000000000000000000 ) ) ;
#672=ORIENTED_EDGE ( 'NONE', *, *, #13406, .T. ) ;
#681=VERTEX_POINT ( 'NONE', #58733 ) ;
#697=CARTESIAN_POINT ( 'NONE',  ( -33.26980702001004175, -9.137952730708951421, -3.992206423873327914 ) ) ;
#702=EDGE_CURVE ( 'NONE', #13056, #23284, #24257, .T. ) ;
#707=B_SPLINE_CURVE_WITH_KNOTS ( 'NONE', 3,
 ( #58669, #36586, #58006, #10500 ),
 .UNSPECIFIED., .F., .F.,
 ( 4, 4 ),
 ( -1.393623722524901192E-05, 0.002366665958592541717 ),
 .UNSPECIFIED. ) ;
#713=CARTESIAN_POINT ( 'NONE',  ( -31.74882385472577084, -8.677117902359153589, -1.656194935354385001 ) ) ;
#717=ORIENTED_EDGE ( 'NONE', *, *, #61031, .T. ) ;
#733=VECTOR ( 'NONE', #5421, 1000.000000000000000 ) ;
#736=CARTESIAN_POINT ( 'NONE',  ( -45.13832304515305083, -13.94474245745556473, 2.675331246431452925 ) ) ;
#737=VERTEX_POINT ( 'NONE', #928 ) ;
#779=CARTESIAN_POINT ( 'NONE',  ( -30.38025804287905629, -8.499999999999996447, -2.000000000000000000 ) ) ;
#807=EDGE_CURVE ( 'NONE', #48124, #69054, #39378, .T. ) ;
#810=CARTESIAN_POINT ( 'NONE',  ( -56.89247722676302033, -8.499999999999992895, -0.08128311974370756865 ) ) ;
#840=LINE ( 'NONE', #28680, #24983 ) ;
#847=EDGE_LOOP ( 'NONE', ( #26581, #32418, #27548, #41432 ) ) ;
#850=EDGE_CURVE ( 'NONE', #23192, #29847, #37737, .T. ) ;
#859=STYLED_ITEM ( 'NONE', ( #4112 ), #4071 ) ;
#913=ORIENTED_EDGE ( 'NONE', *, *, #57118, .F. ) ;
#928=CARTESIAN_POINT ( 'NONE',  ( -12.74999999999999822, -4.000000000000000000, 7.000000000000001776 ) ) ;
#930=DIRECTION ( 'NONE',  ( 1.000000000000000000, 0.000000000000000000, 0.000000000000000000 ) ) ;
#931=ORIENTED_EDGE ( 'NONE', *, *, #25197, .F. ) ;
#1009=CARTESIAN_POINT ( 'NONE',  ( -55.09946728320541354, -8.921903058037614187, -1.645666659141976407 ) ) ;
#1018=CARTESIAN_POINT ( 'NONE',  ( -53.26511667252331250, -9.007918291183415249, 5.430249810268242605 ) ) ;
#1098=PLANE ( 'NONE',  #39875 ) ;
#1115=ORIENTED_EDGE ( 'NONE', *, *, #63135, .T. ) ;
#1127=ORIENTED_EDGE ( 'NONE', *, *, #27155, .F. ) ;
#1134=CARTESIAN_POINT ( 'NONE',  ( -57.58629378005873889, -7.761720733523185700, -0.7755720678490086728 ) ) ;
#1222=ORIENTED_EDGE ( 'NONE', *, *, #587, .F. ) ;
#1252=CARTESIAN_POINT ( 'NONE',  ( -35.35889534745761864, -11.21033625376975529, 1.846521352861608012 ) ) ;
#1298=ORIENTED_EDGE ( 'NONE', *, *, #53745, .F. ) ;
#1310=CYLINDRICAL_SURFACE ( 'NONE', #5308, 1.000000000000000888 ) ;
#1337=CARTESIAN_POINT ( 'NONE',  ( -58.75000000000000000, -8.499999999999992895, 11.89999999999999680 ) ) ;
#1383=CARTESIAN_POINT ( 'NONE',  ( -55.32330819037883174, -8.822438139991119144, -1.968259336913087409 ) ) ;
#1390=ORIENTED_EDGE ( 'NONE', *, *, #3863, .F. ) ;
#1400=CIRCLE ( 'NONE', #49772, 8.999999999999994671 ) ;
#1406=VERTEX_POINT ( 'NONE', #6134 ) ;
#1452=EDGE_CURVE ( 'NONE', #47861, #21323, #48748, .T. ) ;
#1453=CARTESIAN_POINT ( 'NONE',  ( -87.50000000000000000, -8.499999999999989342, 23.00000000000000000 ) ) ;
#1474=LINE ( 'NONE', #45858, #51256 ) ;
#1475=CARTESIAN_POINT ( 'NONE',  ( 3.851859888774471706E-31, -8.500000000000000000, 0.000000000000000000 ) ) ;
#1477=AXIS2_PLACEMENT_3D ( 'NONE', #12607, #18245, #55875 ) ;
#1482=VECTOR ( 'NONE', #10807, 1000.000000000000000 ) ;
#1501=DIRECTION ( 'NONE',  ( -1.000000000000000000, 1.445602896647339656E-16, -0.000000000000000000 ) ) ;
#1520=EDGE_LOOP ( 'NONE', ( #57365, #40556, #39529, #17385 ) ) ;
#1558=ORIENTED_EDGE ( 'NONE', *, *, #27850, .F. ) ;
#1562=ORIENTED_EDGE ( 'NONE', *, *, #47547, .T. ) ;
#1608=CARTESIAN_POINT ( 'NONE',  ( -38.76790784220121111, -11.41832517657503487, 3.451608923803376250 ) ) ;
#1646=ORIENTED_EDGE ( 'NONE', *, *, #26508, .F. ) ;
#1676=CARTESIAN_POINT ( 'NONE',  ( -40.66823730937047543, -13.67203837763575436, 0.8500273690653776804 ) ) ;
#1686=DIRECTION ( 'NONE',  ( 0.000000000000000000, 1.000000000000000000, 0.000000000000000000 ) ) ;
#1718=AXIS2_PLACEMENT_3D ( 'NONE', #43200, #48810, #44230 ) ;
#1738=AXIS2_PLACEMENT_3D ( 'NONE', #27033, #21799, #43312 ) ;
#1787=CARTESIAN_POINT ( 'NONE',  ( -33.13898406348611303, -9.269969315817824906, -2.682282538649360504 ) ) ;
#1828=VERTEX_POINT ( 'NONE', #24633 ) ;
#1832=DIRECTION ( 'NONE',  ( 0.000000000000000000, 0.000000000000000000, -1.000000000000000000 ) ) ;
#1834=CARTESIAN_POINT ( 'NONE',  ( -48.09626709540965095, -13.32227690487224692, 2.730064154176659041 ) ) ;
#1842=EDGE_CURVE ( 'NONE', #17714, #62163, #39146, .T. ) ;
#1849=CARTESIAN_POINT ( 'NONE',  ( -54.73148258177910463, -9.107254030097818642, -1.999999999999995781 ) ) ;
#1874=CARTESIAN_POINT ( 'NONE',  ( -33.89861118948982721, -9.947368421052626530, 2.722470280083843619 ) ) ;
#1875=CARTESIAN_POINT ( 'NONE',  ( -75.75000000000000000, -0.9999999999999995559, 20.00000000000000000 ) ) ;
#1908=ADVANCED_FACE ( 'NONE', ( #63674 ), #26026, .T. ) ;
#1915=LINE ( 'NONE', #39647, #67942 ) ;
#1921=CARTESIAN_POINT ( 'NONE',  ( -30.38025804287905629, -8.499999999999996447, 8.000000000000000000 ) ) ;
#1936=CARTESIAN_POINT ( 'NONE',  ( -37.05138327197616377, -10.73391388307777916, 3.833378626313314275 ) ) ;
#1938=VECTOR ( 'NONE', #22305, 1000.000000000000000 ) ;
#1983=EDGE_CURVE ( 'NONE', #60509, #45120, #1915, .T. ) ;
#1986=DIRECTION ( 'NONE',  ( 1.000000000000000000, 7.703719777548942317E-32, 0.000000000000000000 ) ) ;
#2001=CARTESIAN_POINT ( 'NONE',  ( -30.38025804288019671, -8.499999999999996447, 0.06931351858043485747 ) ) ;
#2013=CARTESIAN_POINT ( 'NONE',  ( -57.66974776420195781, -8.499999999999992895, 0.3730306325211200646 ) ) ;
#2031=AXIS2_PLACEMENT_3D ( 'NONE', #59980, #64904, #28284 ) ;
#2049=EDGE_LOOP ( 'NONE', ( #54857, #54987, #54703, #56535 ) ) ;
#2079=CARTESIAN_POINT ( 'NONE',  ( -47.88739147232087134, -11.66012019292491608, 3.348867242218062312 ) ) ;
#2101=DIRECTION ( 'NONE',  ( 1.000000000000000000, 0.000000000000000000, -0.000000000000000000 ) ) ;
#2137=CARTESIAN_POINT ( 'NONE',  ( -3.000000000000000000, -3.499999999999999556, 0.000000000000000000 ) ) ;
#2161=CARTESIAN_POINT ( 'NONE',  ( -50.15331471893564697, -12.46732336030118482, 2.905981105417522858 ) ) ;
#2218=CARTESIAN_POINT ( 'NONE',  ( -87.50000000000000000, -8.499999999999989342, 21.00000000000000000 ) ) ;
#2285=CARTESIAN_POINT ( 'NONE',  ( -71.75000000000000000, -4.000000000000000000, 19.00000000000000000 ) ) ;
#2349=CARTESIAN_POINT ( 'NONE',  ( -47.09072696197004149, -13.61106737609491013, 0.8658857160018818000 ) ) ;
#2398=VERTEX_POINT ( 'NONE', #2137 ) ;
#2443=CARTESIAN_POINT ( 'NONE',  ( -47.00571487472603138, -11.85301361210301607, 3.279042910798483312 ) ) ;
#2475=CARTESIAN_POINT ( 'NONE',  ( -74.75000000000000000, -4.000000000000000000, 6.000000000000001776 ) ) ;
#2488=VERTEX_POINT ( 'NONE', #47971 ) ;
#2522=FACE_OUTER_BOUND ( 'NONE', #4551, .T. ) ;
#2529=LINE ( 'NONE', #24036, #44107 ) ;
#2534=CARTESIAN_POINT ( 'NONE',  ( -50.85337874892448440, -12.07627951188113080, 3.038067889716521197 ) ) ;
#2583=CARTESIAN_POINT ( 'NONE',  ( -53.18756747357285519, -10.02680648607945102, -3.500000000000002220 ) ) ;
#2594=ORIENTED_EDGE ( 'NONE', *, *, #35095, .T. ) ;
#2669=LINE ( 'NONE', #25209, #37108 ) ;
#2686=VECTOR ( 'NONE', #230, 1000.000000000000000 ) ;
#2692=( BOUNDED_CURVE ( )  B_SPLINE_CURVE ( 3, ( #69229, #57268, #4843, #21027 ),
 .UNSPECIFIED., .F., .F. ) 
 B_SPLINE_CURVE_WITH_KNOTS ( ( 4, 4 ),
 ( 4.712388980384689674, 6.283185307179586232 ),
 .UNSPECIFIED. ) 
 CURVE ( )  GEOMETRIC_REPRESENTATION_ITEM ( )  RATIONAL_B_SPLINE_CURVE ( ( 1.000000000000000000, 0.8047378541243649375, 0.8047378541243649375, 1.000000000000000000 ) ) 
 REPRESENTATION_ITEM ( '' )  );
#2704=CARTESIAN_POINT ( 'NONE',  ( -28.74999999999999645, -13.99999999999999822, 15.00000000000000178 ) ) ;
#2743=CARTESIAN_POINT ( 'NONE',  ( -27.42382197899661733, -8.499999999999996447, 0.9999999970521835646 ) ) ;
#2754=AXIS2_PLACEMENT_3D ( 'NONE', #7842, #23677, #45537 ) ;
#2758=DIRECTION ( 'NONE',  ( 0.000000000000000000, 0.000000000000000000, -1.000000000000000000 ) ) ;
#2802=CIRCLE ( 'NONE', #6201, 1.999999999999998224 ) ;
#2807=CARTESIAN_POINT ( 'NONE',  ( -31.52128483857211094, -8.189042938456932319, -1.771464601026943919 ) ) ;
#2808=LINE ( 'NONE', #67563, #45317 ) ;
#2828=CARTESIAN_POINT ( 'NONE',  ( -32.56443198605217049, -8.762778093183483108, -2.500000000007921219 ) ) ;
#2845=AXIS2_PLACEMENT_3D ( 'NONE', #31993, #32333, #53784 ) ;
#2852=EDGE_LOOP ( 'NONE', ( #11947, #41861, #63495, #26806, #53757, #4081, #31832, #17738, #18764, #20242, #34660, #31018, #42870, #39980, #1127, #53447, #37758, #60704 ) ) ;
#2887=ORIENTED_EDGE ( 'NONE', *, *, #37565, .F. ) ;
#2900=CIRCLE ( 'NONE', #15197, 1.000000000000000000 ) ;
#2924=ORIENTED_EDGE ( 'NONE', *, *, #57553, .F. ) ;
#3006=CIRCLE ( 'NONE', #7583, 1.000000000000000000 ) ;
#3036=ORIENTED_EDGE ( 'NONE', *, *, #57249, .T. ) ;
#3135=ORIENTED_EDGE ( 'NONE', *, *, #14381, .T. ) ;
#3140=CARTESIAN_POINT ( 'NONE',  ( -25.21060798583054563, 0.000000000000000000, -5.000000000000000000 ) ) ;
#3177=ORIENTED_EDGE ( 'NONE', *, *, #65268, .F. ) ;
#3183=CARTESIAN_POINT ( 'NONE',  ( -57.11974195711956526, -8.499999999999992895, 0.06931351858043294234 ) ) ;
#3238=DIRECTION ( 'NONE',  ( -0.000000000000000000, 1.000000000000000000, 0.000000000000000000 ) ) ;
#3247=AXIS2_PLACEMENT_3D ( 'NONE', #58499, #48003, #43423 ) ;
#3277=ADVANCED_FACE ( 'NONE', ( #63895 ), #26270, .T. ) ;
#3298=CARTESIAN_POINT ( 'NONE',  ( -28.74999999999999645, -4.000000000000000000, 11.89999999999999680 ) ) ;
#3313=DIRECTION ( 'NONE',  ( -1.000000000000000000, 1.445602896647339656E-16, 0.000000000000000000 ) ) ;
#3327=CIRCLE ( 'NONE', #31427, 1.000000000000000000 ) ;
#3347=DIRECTION ( 'NONE',  ( 0.000000000000000000, 0.000000000000000000, -1.000000000000000000 ) ) ;
#3379=AXIS2_PLACEMENT_3D ( 'NONE', #37250, #68886, #15431 ) ;
#3382=VERTEX_POINT ( 'NONE', #63739 ) ;
#3389=CARTESIAN_POINT ( 'NONE',  ( -53.56549681293840592, -9.954220776862749531, -2.519071624164535450 ) ) ;
#3393=VERTEX_POINT ( 'NONE', #18830 ) ;
#3481=AXIS2_PLACEMENT_3D ( 'NONE', #9883, #62972, #14815 ) ;
#3527=VERTEX_POINT ( 'NONE', #10639 ) ;
#3607=ADVANCED_FACE ( 'NONE', ( #64792 ), #3969, .F. ) ;
#3614=EDGE_CURVE ( 'NONE', #62964, #48775, #59183, .T. ) ;
#3664=EDGE_CURVE ( 'NONE', #13056, #33368, #4869, .T. ) ;
#3718=EDGE_CURVE ( 'NONE', #66384, #68588, #3006, .T. ) ;
#3727=CIRCLE ( 'NONE', #25112, 3.100000000000005418 ) ;
#3758=SURFACE_STYLE_USAGE ( .BOTH. , #62865 ) ;
#3863=EDGE_CURVE ( 'NONE', #737, #56578, #49579, .T. ) ;
#3865=CARTESIAN_POINT ( 'NONE',  ( -53.22588732449509763, -10.24482008810577582, 4.106145367375290789 ) ) ;
#3905=ADVANCED_FACE ( 'NONE', ( #22141 ), #1310, .F. ) ;
#3910=DIRECTION ( 'NONE',  ( 0.000000000000000000, 1.000000000000000000, 0.000000000000000000 ) ) ;
#3914=EDGE_CURVE ( 'NONE', #42263, #17125, #12043, .T. ) ;
#3951=CARTESIAN_POINT ( 'NONE',  ( -74.75000000000000000, -3.000000000000000000, 7.000000000000001776 ) ) ;
#3958=LINE ( 'NONE', #25432, #64214 ) ;
#3960=ADVANCED_FACE ( 'NONE', ( #65399 ), #10559, .F. ) ;
#3962=ORIENTED_EDGE ( 'NONE', *, *, #29145, .F. ) ;
#3969=( BOUNDED_SURFACE ( )  B_SPLINE_SURFACE ( 3, 2, ( 
 ( #27813, #32780, #38099 ),
 ( #48662, #49664, #59859 ),
 ( #12340, #43723, #16632 ),
 ( #21892, #11320, #28151 ),
 ( #10268, #26777, #44435 ),
 ( #697, #49317, #33475 ) ),
 .UNSPECIFIED., .F., .F., .F. ) 
 B_SPLINE_SURFACE_WITH_KNOTS ( ( 4, 2, 4 ),
 ( 3, 3 ),
 ( 0.03640205491000769039, 0.03794596731985265536, 0.03948987972969762034 ),
 ( 0.6341638506276230380, 1.000000000000000000 ),
 .UNSPECIFIED. ) 
 GEOMETRIC_REPRESENTATION_ITEM ( )  RATIONAL_B_SPLINE_SURFACE ( (
 ( 0.9651092272895998025, 0.9724907272183133111, 1.000000000000000000),
 ( 0.9651083974483595229, 0.9724900729384773346, 1.000000000000000000),
 ( 0.9649374241050432399, 0.9723552707551401664, 1.000000000000000000),
 ( 0.9642640192915807873, 0.9718243316194610237, 1.000000000000000000),
 ( 0.9637558210279215665, 0.9714236478977728018, 1.000000000000000000),
 ( 0.9630880506049159795, 0.9708971511396047305, 1.000000000000000000) ) ) 
 REPRESENTATION_ITEM ( '' )  SURFACE ( )  );
#3992=LINE ( 'NONE', #52576, #60447 ) ;
#3998=CYLINDRICAL_SURFACE ( 'NONE', #33778, 1.000000000000000000 ) ;
#4002=CARTESIAN_POINT ( 'NONE',  ( -75.75000000000000000, -4.000000000000000000, 19.00000000000000000 ) ) ;
#4033=CARTESIAN_POINT ( 'NONE',  ( 3.851859888774471706E-31, -8.500000000000000000, 24.00000000000000000 ) ) ;
#4071=MANIFOLD_SOLID_BREP ( 'Fillet7', #55362 ) ;
#4081=ORIENTED_EDGE ( 'NONE', *, *, #29447, .F. ) ;
#4112=PRESENTATION_STYLE_ASSIGNMENT (( #3758 ) ) ;
#4137=LINE ( 'NONE', #53063, #63890 ) ;
#4208=EDGE_LOOP ( 'NONE', ( #12232, #49943, #26696, #16542 ) ) ;
#4254=VERTEX_POINT ( 'NONE', #32965 ) ;
#4264=EDGE_CURVE ( 'NONE', #33970, #3527, #42567, .T. ) ;
#4277=CARTESIAN_POINT ( 'NONE',  ( -26.79538245034556709, -8.499999999999996447, 1.000000000000000000 ) ) ;
#4331=( BOUNDED_SURFACE ( )  B_SPLINE_SURFACE ( 3, 2, ( 
 ( #3183, #24676, #53520 ),
 ( #36343, #37392, #26078 ),
 ( #21149, #68669, #20467 ),
 ( #57409, #46561, #35964 ),
 ( #67984, #9234, #31012 ),
 ( #63021, #5302, #52162 ) ),
 .UNSPECIFIED., .F., .F., .F. ) 
 B_SPLINE_SURFACE_WITH_KNOTS ( ( 4, 2, 4 ),
 ( 3, 3 ),
 ( 1.549108064047288735E-15, 0.001858363558057203775, 0.003716727116112858442 ),
 ( 0.000000000000000000, 1.000000000000000000 ),
 .UNSPECIFIED. ) 
 GEOMETRIC_REPRESENTATION_ITEM ( )  RATIONAL_B_SPLINE_SURFACE ( (
 ( 1.000000000000000000, 0.7942671885213775651, 1.000000000000000000),
 ( 1.000000000000000000, 0.7793712970752797453, 1.000000000000000000),
 ( 1.000000000000000000, 0.7645460165485118420, 1.000000000000000000),
 ( 1.000000000000000000, 0.7352674701534978041, 1.000000000000000000),
 ( 1.000000000000000000, 0.7207339695077151775, 1.000000000000000000),
 ( 1.000000000000000000, 0.7071067811865475727, 1.000000000000000000) ) ) 
 REPRESENTATION_ITEM ( '' )  SURFACE ( )  );
#4358=ORIENTED_EDGE ( 'NONE', *, *, #23428, .T. ) ;
#4365=DIRECTION ( 'NONE',  ( 1.000000000000000000, 7.703719777548942317E-32, 0.000000000000000000 ) ) ;
#4413=CIRCLE ( 'NONE', #60558, 1.000000000000000000 ) ;
#4421=CARTESIAN_POINT ( 'NONE',  ( -74.75000000000000000, -4.000000000000000000, 18.00000000000000000 ) ) ;
#4450=EDGE_LOOP ( 'NONE', ( #60189, #48257, #8666, #6151 ) ) ;
#4459=FILL_AREA_STYLE ('',( #67828 ) ) ;
#4461=CARTESIAN_POINT ( 'NONE',  ( -35.65778776279520912, -9.947368421052630083, 4.481646853389227303 ) ) ;
#4470=CARTESIAN_POINT ( 'NONE',  ( -45.96823954197535045, -12.05717624383679087, 3.207817295096130561 ) ) ;
#4551=EDGE_LOOP ( 'NONE', ( #49049, #66038, #717, #65347, #64530, #68335 ) ) ;
#4570=CARTESIAN_POINT ( 'NONE',  ( -53.38227578680366037, -9.152876382972605640, 5.508355886455341022 ) ) ;
#4575=VERTEX_POINT ( 'NONE', #5770 ) ;
#4626=ORIENTED_EDGE ( 'NONE', *, *, #24067, .F. ) ;
#4686=( BOUNDED_SURFACE ( )  B_SPLINE_SURFACE ( 3, 2, ( 
 ( #15085, #15427, #4461 ),
 ( #58302, #31559, #36885 ),
 ( #57975, #5170, #63911 ),
 ( #53039, #46771, #48137 ),
 ( #68519, #68182, #20317 ),
 ( #26616, #31201, #69544 ),
 ( #21348, #19960, #60030 ),
 ( #32967, #54734, #39303 ) ),
 .UNSPECIFIED., .F., .F., .F. ) 
 B_SPLINE_SURFACE_WITH_KNOTS ( ( 4, 2, 2, 4 ),
 ( 3, 3 ),
 ( 3.931838538365183044, 4.126976148870059369, 4.322113759374936137, 4.712388980384689674 ),
 ( 0.000000000000000000, 1.000000000000000000 ),
 .UNSPECIFIED. ) 
 GEOMETRIC_REPRESENTATION_ITEM ( )  RATIONAL_B_SPLINE_SURFACE ( (
 ( 1.000000000000000000, 0.8674236696762900323, 1.000000000000000000),
 ( 1.000000000000000000, 0.8861805033181661129, 1.000000000000000000),
 ( 1.000000000000000000, 0.9042436661780808294, 1.000000000000000000),
 ( 1.000000000000000000, 0.9367862960115365123, 1.000000000000000000),
 ( 1.000000000000000000, 0.9512556414920706471, 1.000000000000000000),
 ( 1.000000000000000000, 0.9868976895440315644, 1.000000000000000000),
 ( 1.000000000000000000, 1.000154660590196087, 1.000000000000000000),
 ( 1.000000000000000000, 1.000000000000000000, 1.000000000000000000) ) ) 
 REPRESENTATION_ITEM ( '' )  SURFACE ( )  );
#4709=FACE_OUTER_BOUND ( 'NONE', #39849, .T. ) ;
#4834=B_SPLINE_CURVE_WITH_KNOTS ( 'NONE', 3,
 ( #37268, #53415, #69569, #5195, #15112, #26637, #21372, #34281, #45577, #12818 ),
 .UNSPECIFIED., .F., .F.,
 ( 4, 2, 2, 2, 4 ),
 ( 0.000000000000000000, 0.001409835084339927094, 0.002819670168679854188, 0.004229505253019781065, 0.005639340337359708376 ),
 .UNSPECIFIED. ) ;
#4843=CARTESIAN_POINT ( 'NONE',  ( -11.74999999999999467, -0.4142135623730948124, 19.00000000000000000 ) ) ;
#4869=B_SPLINE_CURVE_WITH_KNOTS ( 'NONE', 3,
 ( #66526, #62284, #45793, #2807, #67213, #40510, #50696, #12697 ),
 .UNSPECIFIED., .F., .F.,
 ( 4, 2, 2, 4 ),
 ( 0.000000000000000000, 0.001659144101464961850, 0.002488716152197438004, 0.003318288202929914159 ),
 .UNSPECIFIED. ) ;
#4901=ORIENTED_EDGE ( 'NONE', *, *, #7483, .F. ) ;
#4930=ORIENTED_EDGE ( 'NONE', *, *, #57660, .T. ) ;
#4938=ADVANCED_FACE ( 'NONE', ( #27146 ), #16, .F. ) ;
#4940=CARTESIAN_POINT ( 'NONE',  ( -30.38025804287905629, -8.499999999999996447, 0.06931351858032895608 ) ) ;
#4946=FACE_OUTER_BOUND ( 'NONE', #34124, .T. ) ;
#4970=ORIENTED_EDGE ( 'NONE', *, *, #61100, .T. ) ;
#4973=CIRCLE ( 'NONE', #399, 0.9999999999999978906 ) ;
#4976=ORIENTED_EDGE ( 'NONE', *, *, #30117, .F. ) ;
#4978=CIRCLE ( 'NONE', #62324, 1.000000000000000000 ) ;
#5014=ORIENTED_EDGE ( 'NONE', *, *, #54583, .T. ) ;
#5026=ADVANCED_FACE ( 'NONE', ( #67480 ), #45320, .T. ) ;
#5048=AXIS2_PLACEMENT_3D ( 'NONE', #13992, #58206, #10029 ) ;
#5054=FACE_BOUND ( 'NONE', #65714, .T. ) ;
#5071=ORIENTED_EDGE ( 'NONE', *, *, #108, .T. ) ;
#5076=CARTESIAN_POINT ( 'NONE',  ( -74.75000000000000000, -3.000000000000000000, 7.000000000000001776 ) ) ;
#5089=CARTESIAN_POINT ( 'NONE',  ( -43.75000000000000000, 0.000000000000000000, -5.000000000000000000 ) ) ;
#5093=ORIENTED_EDGE ( 'NONE', *, *, #15996, .F. ) ;
#5170=CARTESIAN_POINT ( 'NONE',  ( -34.01240315408732329, -9.962924773521290689, 4.367854888791723234 ) ) ;
#5179=DIRECTION ( 'NONE',  ( 0.000000000000000000, 1.000000000000000000, -0.000000000000000000 ) ) ;
#5195=CARTESIAN_POINT ( 'NONE',  ( -38.88671403932455206, -11.45492897060496240, 3.435370330900509916 ) ) ;
#5203=PLANE ( 'NONE',  #50593 ) ;
#5224=EDGE_LOOP ( 'NONE', ( #24717, #5900, #9626, #63987 ) ) ;
#5230=EDGE_CURVE ( 'NONE', #40317, #57439, #63533, .T. ) ;
#5302=CARTESIAN_POINT ( 'NONE',  ( -60.70461754965442935, -8.499999999999994671, 2.168404344971008868E-16 ) ) ;
#5303=AXIS2_PLACEMENT_3D ( 'NONE', #59009, #36571, #10824 ) ;
#5308=AXIS2_PLACEMENT_3D ( 'NONE', #65029, #32338, #621 ) ;
#5309=VERTEX_POINT ( 'NONE', #22070 ) ;
#5343=VERTEX_POINT ( 'NONE', #26956 ) ;
#5347=EDGE_LOOP ( 'NONE', ( #42508, #19590, #36681 ) ) ;
#5349=DIRECTION ( 'NONE',  ( 1.000000000000000000, 0.000000000000000000, -0.000000000000000000 ) ) ;
#5354=DIRECTION ( 'NONE',  ( -1.000000000000000000, 0.000000000000000000, 0.000000000000000000 ) ) ;
#5368=SHAPE_REPRESENTATION_RELATIONSHIP ( 'NONE' , 'NONE' ,  #22166, #175 ) ;
#5372=CARTESIAN_POINT ( 'NONE',  ( -43.24699869027381993, -14.00614972214689047, 0.7701856363860615229 ) ) ;
#5380=( NAMED_UNIT ( * ) PLANE_ANGLE_UNIT ( ) SI_UNIT ( $, .RADIAN. ) );
#5394=ORIENTED_EDGE ( 'NONE', *, *, #26451, .T. ) ;
#5400=VECTOR ( 'NONE', #17434, 1000.000000000000000 ) ;
#5403=CARTESIAN_POINT ( 'NONE',  ( -33.89861118948983432, -9.947368421052626530, -2.264547950182262070 ) ) ;
#5417=CARTESIAN_POINT ( 'NONE',  ( -87.50000000000000000, -3.500000000000000000, 24.00000000000000000 ) ) ;
#5421=DIRECTION ( 'NONE',  ( 0.000000000000000000, 0.000000000000000000, -1.000000000000000000 ) ) ;
#5472=DIRECTION ( 'NONE',  ( 1.189524669241239115E-16, 1.000000000000000000, 0.000000000000000000 ) ) ;
#5498=ADVANCED_FACE ( 'NONE', ( #51572 ), #41050, .F. ) ;
#5510=ORIENTED_EDGE ( 'NONE', *, *, #51804, .F. ) ;
#5554=CARTESIAN_POINT ( 'NONE',  ( 0.000000000000000000, -4.000000000000000000, 0.000000000000000000 ) ) ;
#5563=CARTESIAN_POINT ( 'NONE',  ( 0.000000000000000000, -4.000000000000000000, 18.00000000000000000 ) ) ;
#5592=DIRECTION ( 'NONE',  ( 0.000000000000000000, 1.000000000000000000, 0.000000000000000000 ) ) ;
#5617=CARTESIAN_POINT ( 'NONE',  ( -12.74999999999999822, -0.9999999999999995559, 7.000000000000001776 ) ) ;
#5627=CYLINDRICAL_SURFACE ( 'NONE', #58412, 13.99999999999999822 ) ;
#5628=AXIS2_PLACEMENT_3D ( 'NONE', #24685, #45844, #18404 ) ;
#5657=CARTESIAN_POINT ( 'NONE',  ( -54.93556801394916533, -8.762778093182603811, -2.500000000007031709 ) ) ;
#5713=CARTESIAN_POINT ( 'NONE',  ( -33.71543202885159474, -9.630272336294959601, -3.117062350998871967 ) ) ;
#5748=DIRECTION ( 'NONE',  ( -1.000000000000000000, -0.000000000000000000, -0.000000000000000000 ) ) ;
#5770=CARTESIAN_POINT ( 'NONE',  ( -71.75000000000000000, -4.000000000000000000, 18.00000000000000000 ) ) ;
#5796=ORIENTED_EDGE ( 'NONE', *, *, #1452, .F. ) ;
#5841=DIRECTION ( 'NONE',  ( -0.000000000000000000, 1.000000000000000000, -0.000000000000000000 ) ) ;
#5844=DIRECTION ( 'NONE',  ( 0.000000000000000000, 0.000000000000000000, 1.000000000000000000 ) ) ;
#5856=VERTEX_POINT ( 'NONE', #47793 ) ;
#5900=ORIENTED_EDGE ( 'NONE', *, *, #58358, .T. ) ;
#5912=CIRCLE ( 'NONE', #231, 1.000000000000000888 ) ;
#5985=CIRCLE ( 'NONE', #23968, 8.499999999999992895 ) ;
#6003=LINE ( 'NONE', #38059, #26910 ) ;
#6043=ORIENTED_EDGE ( 'NONE', *, *, #7814, .F. ) ;
#6062=AXIS2_PLACEMENT_3D ( 'NONE', #56845, #57533, #58226 ) ;
#6087=CARTESIAN_POINT ( 'NONE',  ( -44.40807425668157293, -12.16242975799924864, 3.182228584415367489 ) ) ;
#6103=CARTESIAN_POINT ( 'NONE',  ( -43.75000000000000000, 0.000000000000000000, -3.499999999999997335 ) ) ;
#6127=ORIENTED_EDGE ( 'NONE', *, *, #332, .F. ) ;
#6134=CARTESIAN_POINT ( 'NONE',  ( -71.75000000000000000, 4.336808689942018722E-16, 20.00000000000000000 ) ) ;
#6151=ORIENTED_EDGE ( 'NONE', *, *, #47413, .F. ) ;
#6156=DIRECTION ( 'NONE',  ( 0.000000000000000000, -1.000000000000000000, 0.000000000000000000 ) ) ;
#6201=AXIS2_PLACEMENT_3D ( 'NONE', #55956, #34843, #50691 ) ;
#6217=ORIENTED_EDGE ( 'NONE', *, *, #43407, .T. ) ;
#6224=B_SPLINE_CURVE_WITH_KNOTS ( 'NONE', 3,
 ( #52934, #64156, #16012, #69444, #58897, #42762, #42418, #52257 ),
 .UNSPECIFIED., .F., .F.,
 ( 4, 2, 2, 4 ),
 ( 4.596172765309288096E-15, 0.0008152109970724930607, 0.001630421994140389972, 0.003260843988276192467 ),
 .UNSPECIFIED. ) ;
#6225=CARTESIAN_POINT ( 'NONE',  ( -10.74999999999999645, 4.336808689942018722E-16, 7.000000000000001776 ) ) ;
#6229=EDGE_LOOP ( 'NONE', ( #17991, #1390, #19875, #25266 ) ) ;
#6271=ORIENTED_EDGE ( 'NONE', *, *, #11480, .F. ) ;
#6292=CARTESIAN_POINT ( 'NONE',  ( -11.99999999999999822, -8.499999999999998224, 21.00000000000000000 ) ) ;
#6315=CARTESIAN_POINT ( 'NONE',  ( -28.94093048474993779, -8.499999999999996447, 0.6846459046698460948 ) ) ;
#6322=DIRECTION ( 'NONE',  ( 0.000000000000000000, 0.000000000000000000, -1.000000000000000000 ) ) ;
#6334=CARTESIAN_POINT ( 'NONE',  ( -9.908575283019912422E-16, -6.500000000000002665, 0.000000000000000000 ) ) ;
#6344=EDGE_CURVE ( 'NONE', #57528, #54598, #51647, .T. ) ;
#6405=CARTESIAN_POINT ( 'NONE',  ( -47.00571487472603138, -11.85301361210301607, 3.279042910798483312 ) ) ;
#6407=DIRECTION ( 'NONE',  ( -0.000000000000000000, 0.000000000000000000, -1.000000000000000000 ) ) ;
#6424=CARTESIAN_POINT ( 'NONE',  ( -41.30498680716012672, -13.80019380139175666, 0.8186576791469339920 ) ) ;
#6495=CYLINDRICAL_SURFACE ( 'NONE', #54762, 1.000000000000000888 ) ;
#6508=LINE ( 'NONE', #2218, #13783 ) ;
#6520=ORIENTED_EDGE ( 'NONE', *, *, #20586, .T. ) ;
#6550=DIRECTION ( 'NONE',  ( 0.000000000000000000, 0.000000000000000000, -1.000000000000000000 ) ) ;
#6568=CARTESIAN_POINT ( 'NONE',  ( -36.30021781998517127, -10.34894320149787816, 4.110481005326708015 ) ) ;
#6594=( BOUNDED_SURFACE ( )  B_SPLINE_SURFACE ( 3, 2, ( 
 ( #20054, #36295, #61929 ),
 ( #58072, #3865, #25349 ),
 ( #41220, #36652, #35217 ),
 ( #4570, #30609, #19370 ),
 ( #51754, #46508, #52112 ),
 ( #68620, #24999, #52461 ),
 ( #40518, #29931, #47199 ),
 ( #19008, #14115, #51393 ) ),
 .UNSPECIFIED., .F., .F., .F. ) 
 B_SPLINE_SURFACE_WITH_KNOTS ( ( 4, 2, 2, 4 ),
 ( 3, 3 ),
 ( 3.931838538365182600, 4.126976148870059369, 4.322113759374936137, 4.712388980384689674 ),
 ( 0.000000000000000000, 1.000000000000000000 ),
 .UNSPECIFIED. ) 
 GEOMETRIC_REPRESENTATION_ITEM ( )  RATIONAL_B_SPLINE_SURFACE ( (
 ( 1.000000000000000000, 0.8674236696762896992, 1.000000000000000000),
 ( 1.000000000000000000, 0.8861805033181393565, 1.000000000000000000),
 ( 1.000000000000000000, 0.9042436661781160234, 1.000000000000000000),
 ( 1.000000000000000000, 0.9367862960115010962, 1.000000000000000000),
 ( 1.000000000000000000, 0.9512556414921075065, 1.000000000000000000),
 ( 1.000000000000000000, 0.9868976895439577346, 1.000000000000000000),
 ( 1.000000000000000000, 1.000154660590251154, 1.000000000000000000),
 ( 1.000000000000000000, 1.000000000000000000, 1.000000000000000000) ) ) 
 REPRESENTATION_ITEM ( '' )  SURFACE ( )  );
#6642=LINE ( 'NONE', #49948, #29187 ) ;
#6656=CARTESIAN_POINT ( 'NONE',  ( -84.49999999999998579, -3.499999999999999556, 0.000000000000000000 ) ) ;
#6685=ORIENTED_EDGE ( 'NONE', *, *, #43497, .F. ) ;
#6726=DIRECTION ( 'NONE',  ( -1.000000000000000000, 0.000000000000000000, 0.000000000000000000 ) ) ;
#6766=CYLINDRICAL_SURFACE ( 'NONE', #39995, 6.000000000000005329 ) ;
#6787=CIRCLE ( 'NONE', #3379, 3.100000000000001865 ) ;
#6809=LINE ( 'NONE', #50101, #1938 ) ;
#6834=CARTESIAN_POINT ( 'NONE',  ( -53.18756747357344494, -10.02680648607920588, -3.499999999999313882 ) ) ;
#6836=CIRCLE ( 'NONE', #21453, 18.53939201416945082 ) ;
#6861=CARTESIAN_POINT ( 'NONE',  ( -55.09822643348442028, -8.922505785858549032, -1.646890977621942254 ) ) ;
#6883=CIRCLE ( 'NONE', #13607, 5.000000000000000000 ) ;
#6919=VERTEX_POINT ( 'NONE', #20304 ) ;
#6937=CARTESIAN_POINT ( 'NONE',  ( -35.96227966833271239, -10.14840438130919331, 4.278652250189864503 ) ) ;
#6938=VECTOR ( 'NONE', #7031, 1000.000000000000000 ) ;
#6959=CARTESIAN_POINT ( 'NONE',  ( -11.99999999999999822, -8.499999999999998224, 21.00000000000000000 ) ) ;
#6961=AXIS2_PLACEMENT_3D ( 'NONE', #4002, #25472, #41693 ) ;
#6993=EDGE_CURVE ( 'NONE', #56449, #17121, #1400, .T. ) ;
#6994=DIRECTION ( 'NONE',  ( -1.000000000000000000, 0.000000000000000000, 0.000000000000000000 ) ) ;
#7021=CARTESIAN_POINT ( 'NONE',  ( -12.74999999999999822, -3.000000000000000000, 6.000000000000001776 ) ) ;
#7031=DIRECTION ( 'NONE',  ( 0.000000000000000000, 0.000000000000000000, -1.000000000000000000 ) ) ;
#7043=CARTESIAN_POINT ( 'NONE',  ( -11.74999999999999645, -0.9999999999999995559, 19.00000000000000000 ) ) ;
#7066=CARTESIAN_POINT ( 'NONE',  ( -56.00691142449380777, -8.176804786315972962, -1.751816976611608512 ) ) ;
#7081=CARTESIAN_POINT ( 'NONE',  ( -11.74999999999999645, 4.336808689942018722E-16, 5.000000000000001776 ) ) ;
#7090=ORIENTED_EDGE ( 'NONE', *, *, #24067, .T. ) ;
#7108=VECTOR ( 'NONE', #56489, 1000.000000000000000 ) ;
#7122=FACE_OUTER_BOUND ( 'NONE', #39514, .T. ) ;
#7180=CARTESIAN_POINT ( 'NONE',  ( -52.31798797533910061, -11.10405175802884159, 3.489986028532363171 ) ) ;
#7190=DIRECTION ( 'NONE',  ( -1.000000000000000000, 0.000000000000000000, 0.000000000000000000 ) ) ;
#7201=CARTESIAN_POINT ( 'NONE',  ( -15.75000000000000000, -3.000000000000000000, 19.00000000000000000 ) ) ;
#7217=DIRECTION ( 'NONE',  ( 0.000000000000000000, 0.000000000000000000, 1.000000000000000000 ) ) ;
#7248=DIRECTION ( 'NONE',  ( 1.000000000000000000, 0.000000000000000000, -0.000000000000000000 ) ) ;
#7252=EDGE_CURVE ( 'NONE', #18813, #19277, #67887, .T. ) ;
#7326=EDGE_CURVE ( 'NONE', #5309, #54365, #28502, .T. ) ;
#7331=ORIENTED_EDGE ( 'NONE', *, *, #35180, .T. ) ;
#7338=ORIENTED_EDGE ( 'NONE', *, *, #47948, .T. ) ;
#7365=ORIENTED_EDGE ( 'NONE', *, *, #25323, .T. ) ;
#7373=CARTESIAN_POINT ( 'NONE',  ( -49.75000000000000000, 4.336808689942018722E-16, 16.97056274847714974 ) ) ;
#7419=ORIENTED_EDGE ( 'NONE', *, *, #24557, .T. ) ;
#7446=CARTESIAN_POINT ( 'NONE',  ( -51.51031159759250500, -10.16650056460914087, 4.260379760314384257 ) ) ;
#7449=EDGE_CURVE ( 'NONE', #24594, #58716, #4973, .T. ) ;
#7483=EDGE_CURVE ( 'NONE', #54909, #36200, #46233, .T. ) ;
#7516=FACE_OUTER_BOUND ( 'NONE', #35631, .T. ) ;
#7564=ADVANCED_FACE ( 'NONE', ( #67651 ), #61644, .T. ) ;
#7583=AXIS2_PLACEMENT_3D ( 'NONE', #14108, #13748, #56667 ) ;
#7607=CARTESIAN_POINT ( 'NONE',  ( -83.49999999999998579, 4.336808689942018722E-16, 24.00000000000000000 ) ) ;
#7613=CARTESIAN_POINT ( 'NONE',  ( -74.75000000000000000, -3.000000000000000000, 6.000000000000001776 ) ) ;
#7629=DIRECTION ( 'NONE',  ( 1.000000000000000000, 0.000000000000000000, 0.000000000000000000 ) ) ;
#7632=LINE ( 'NONE', #2285, #59277 ) ;
#7690=CARTESIAN_POINT ( 'NONE',  ( -32.02155123813385273, -8.772721419152789579, -1.279060632649535290 ) ) ;
#7694=ORIENTED_EDGE ( 'NONE', *, *, #9558, .T. ) ;
#7717=VECTOR ( 'NONE', #55236, 1000.000000000000000 ) ;
#7761=ORIENTED_EDGE ( 'NONE', *, *, #55682, .T. ) ;
#7779=ORIENTED_EDGE ( 'NONE', *, *, #54395, .T. ) ;
#7814=EDGE_CURVE ( 'NONE', #68588, #25847, #19628, .T. ) ;
#7842=CARTESIAN_POINT ( 'NONE',  ( -43.75000000000000000, 0.000000000000000000, -5.000000000000000000 ) ) ;
#7849=CARTESIAN_POINT ( 'NONE',  ( -4.000000000000000000, -3.499999999999999556, 0.000000000000000000 ) ) ;
#7888=ORIENTED_EDGE ( 'NONE', *, *, #31362, .F. ) ;
#7907=( NAMED_UNIT ( * ) PLANE_ANGLE_UNIT ( ) SI_UNIT ( $, .RADIAN. ) );
#7980=CARTESIAN_POINT ( 'NONE',  ( -38.31544721422453392, -11.26485886809405557, 3.523166290182464966 ) ) ;
#7981=VECTOR ( 'NONE', #66752, 1000.000000000000000 ) ;
#7998=AXIS2_PLACEMENT_3D ( 'NONE', #47603, #3910, #9586 ) ;
#8017=ORIENTED_EDGE ( 'NONE', *, *, #43009, .T. ) ;
#8049=CARTESIAN_POINT ( 'NONE',  ( -32.34737067114478037, -8.620612969373077306, -2.355895588769170157 ) ) ;
#8057=LINE ( 'NONE', #7373, #48655 ) ;
#8064=CARTESIAN_POINT ( 'NONE',  ( -28.91386553845895335, -7.667674748043721955, -0.3278848047015802680 ) ) ;
#8221=AXIS2_PLACEMENT_3D ( 'NONE', #60965, #11488, #58991 ) ;
#8326=DIRECTION ( 'NONE',  ( 0.000000000000000000, 0.000000000000000000, 1.000000000000000000 ) ) ;
#8377=ORIENTED_EDGE ( 'NONE', *, *, #67053, .F. ) ;
#8388=VECTOR ( 'NONE', #46808, 1000.000000000000000 ) ;
#8429=CARTESIAN_POINT ( 'NONE',  ( -28.94829758246651252, -8.499999999999996447, -0.1896701972874017816 ) ) ;
#8440=PLANE ( 'NONE',  #52922 ) ;
#8452=LINE ( 'NONE', #57308, #37157 ) ;
#8569=ORIENTED_EDGE ( 'NONE', *, *, #32823, .F. ) ;
#8574=ORIENTED_EDGE ( 'NONE', *, *, #32823, .T. ) ;
#8615=CARTESIAN_POINT ( 'NONE',  ( -53.31913400974866590, -10.00145578784314715, -3.271963658655177021 ) ) ;
#8625=DIRECTION ( 'NONE',  ( -0.000000000000000000, -0.000000000000000000, 1.000000000000000000 ) ) ;
#8639=CARTESIAN_POINT ( 'NONE',  ( -76.75000000000000000, 4.336808689942018722E-16, 20.00000000000000000 ) ) ;
#8643=ORIENTED_EDGE ( 'NONE', *, *, #32236, .F. ) ;
#8666=ORIENTED_EDGE ( 'NONE', *, *, #30569, .F. ) ;
#8722=CARTESIAN_POINT ( 'NONE',  ( -54.10982952226344622, -9.443833522991335272, -2.300020890959020736 ) ) ;
#8728=ORIENTED_EDGE ( 'NONE', *, *, #67682, .F. ) ;
#8734=DIRECTION ( 'NONE',  ( 1.000000000000000000, -0.000000000000000000, 0.000000000000000000 ) ) ;
#8737=CARTESIAN_POINT ( 'NONE',  ( -47.71347897792733761, -13.42724224818812040, 0.9185643661977238583 ) ) ;
#8745=CARTESIAN_POINT ( 'NONE',  ( -32.17428486863278181, -8.821435577490872149, -1.966464606294938910 ) ) ;
#8780=DIRECTION ( 'NONE',  ( 1.000000000000000000, 0.000000000000000000, 0.000000000000000000 ) ) ;
#8782=ORIENTED_EDGE ( 'NONE', *, *, #59566, .F. ) ;
#8796=LINE ( 'NONE', #46475, #51559 ) ;
#8822=CARTESIAN_POINT ( 'NONE',  ( 3.081487911019577365E-31, -7.500000000000000888, 0.000000000000000000 ) ) ;
#8835=ORIENTED_EDGE ( 'NONE', *, *, #49042, .F. ) ;
#8838=EDGE_CURVE ( 'NONE', #20367, #19782, #68111, .T. ) ;
#8840=EDGE_CURVE ( 'NONE', #14317, #13056, #47318, .T. ) ;
#8842=PLANE ( 'NONE',  #66808 ) ;
#8892=AXIS2_PLACEMENT_3D ( 'NONE', #66550, #13414, #46168 ) ;
#8917=EDGE_CURVE ( 'NONE', #3393, #61550, #26255, .T. ) ;
#8935=CIRCLE ( 'NONE', #48278, 1.000000000000000888 ) ;
#8941=DIRECTION ( 'NONE',  ( -1.189524669241239115E-16, -1.000000000000000000, -0.000000000000000000 ) ) ;
#8991=CARTESIAN_POINT ( 'NONE',  ( -34.23488332747668750, -9.007918291183415249, 5.430249810268243493 ) ) ;
#8997=ADVANCED_FACE ( 'NONE', ( #63873 ), #53351, .F. ) ;
#9011=ADVANCED_FACE ( 'NONE', ( #22027 ), #21667, .F. ) ;
#9025=CARTESIAN_POINT ( 'NONE',  ( -11.74999999999999645, -3.000000000000000000, 7.000000000000001776 ) ) ;
#9030=CARTESIAN_POINT ( 'NONE',  ( -40.20684803154669851, -11.80180942591514182, 3.296236230148514856 ) ) ;
#9044=VECTOR ( 'NONE', #66664, 1000.000000000000000 ) ;
#9136=AXIS2_PLACEMENT_3D ( 'NONE', #52047, #41161, #46810 ) ;
#9234=CARTESIAN_POINT ( 'NONE',  ( -60.17648784341465529, -8.499999999999994671, 0.03783916848062766208 ) ) ;
#9335=CARTESIAN_POINT ( 'NONE',  ( -35.63345864320083223, -11.41101942758246857, 1.735234313984338694 ) ) ;
#9401=EDGE_CURVE ( 'NONE', #29467, #48775, #69106, .T. ) ;
#9411=DIRECTION ( 'NONE',  ( 1.189524669241239115E-16, 1.000000000000000000, 0.000000000000000000 ) ) ;
#9440=CARTESIAN_POINT ( 'NONE',  ( -8.921435019309294474E-16, -7.500000000000000888, 0.000000000000000000 ) ) ;
#9466=EDGE_CURVE ( 'NONE', #22579, #11830, #42066, .T. ) ;
#9483=DIRECTION ( 'NONE',  ( -1.000000000000000000, 0.000000000000000000, 0.000000000000000000 ) ) ;
#9558=EDGE_CURVE ( 'NONE', #29573, #56578, #49366, .T. ) ;
#9586=DIRECTION ( 'NONE',  ( 0.000000000000000000, 0.000000000000000000, 1.000000000000000000 ) ) ;
#9626=ORIENTED_EDGE ( 'NONE', *, *, #69129, .F. ) ;
#9657=VECTOR ( 'NONE', #35548, 1000.000000000000000 ) ;
#9698=CARTESIAN_POINT ( 'NONE',  ( -59.62249556327051891, -7.581530822753633991, -0.08527172969607607622 ) ) ;
#9715=DIRECTION ( 'NONE',  ( 0.000000000000000000, 0.000000000000000000, 1.000000000000000000 ) ) ;
#9748=LINE ( 'NONE', #54005, #63465 ) ;
#9806=ORIENTED_EDGE ( 'NONE', *, *, #41330, .T. ) ;
#9826=CARTESIAN_POINT ( 'NONE',  ( -58.75000000000000000, -13.99999999999999822, 15.00000000000000178 ) ) ;
#9836=ORIENTED_EDGE ( 'NONE', *, *, #38638, .T. ) ;
#9851=EDGE_LOOP ( 'NONE', ( #4970, #67115, #30222, #46798 ) ) ;
#9883=CARTESIAN_POINT ( 'NONE',  ( -7.731910350068054619E-16, -6.500000000000000888, 3.000000000000000000 ) ) ;
#9884=CARTESIAN_POINT ( 'NONE',  ( 2.311115933264683462E-31, -6.500000000000000888, 3.000000000000002665 ) ) ;
#9909=LINE ( 'NONE', #41580, #68524 ) ;
#9925=CARTESIAN_POINT ( 'NONE',  ( 0.000000000000000000, -3.500000000000000000, 24.00000000000000000 ) ) ;
#9931=ORIENTED_EDGE ( 'NONE', *, *, #7326, .T. ) ;
#9964=VECTOR ( 'NONE', #23363, 1000.000000000000000 ) ;
#9965=EDGE_CURVE ( 'NONE', #22579, #54909, #22550, .T. ) ;
#9999=LINE ( 'NONE', #58877, #59683 ) ;
#10003=DIRECTION ( 'NONE',  ( -1.189524669241239115E-16, -1.000000000000000000, 0.000000000000000000 ) ) ;
#10026=VERTEX_POINT ( 'NONE', #40145 ) ;
#10029=DIRECTION ( 'NONE',  ( 0.000000000000000000, 0.000000000000000000, 1.000000000000000000 ) ) ;
#10033=ORIENTED_EDGE ( 'NONE', *, *, #26187, .T. ) ;
#10039=FACE_OUTER_BOUND ( 'NONE', #31821, .T. ) ;
#10044=DIRECTION ( 'NONE',  ( 1.000000000000000000, -0.000000000000000000, 0.000000000000000000 ) ) ;
#10070=B_SPLINE_CURVE_WITH_KNOTS ( 'NONE', 3,
 ( #28298, #39271, #24098, #50493, #44900, #23393, #28664, #13183 ),
 .UNSPECIFIED., .F., .F.,
 ( 4, 2, 2, 4 ),
 ( 0.000000000000000000, 0.001660002979567827509, 0.002490004469351742022, 0.003320005959135656319 ),
 .UNSPECIFIED. ) ;
#10106=ORIENTED_EDGE ( 'NONE', *, *, #47963, .F. ) ;
#10119=EDGE_CURVE ( 'NONE', #22278, #38572, #8796, .T. ) ;
#10159=CARTESIAN_POINT ( 'NONE',  ( -87.50000000000000000, -8.499999999999989342, 23.00000000000000000 ) ) ;
#10194=DIRECTION ( 'NONE',  ( 1.000000000000000000, 0.000000000000000000, -0.000000000000000000 ) ) ;
#10206=CARTESIAN_POINT ( 'NONE',  ( -30.38025804288030329, -7.499999999999996447, 0.06931351858050209536 ) ) ;
#10231=CARTESIAN_POINT ( 'NONE',  ( -37.74999999999999289, 4.336808689942018722E-16, 16.97056274847714974 ) ) ;
#10236=CARTESIAN_POINT ( 'NONE',  ( -87.50000000000000000, -6.499999999999990230, 3.000000000000000000 ) ) ;
#10268=CARTESIAN_POINT ( 'NONE',  ( -33.10370830234652573, -9.126466545927527818, -3.681448577161279712 ) ) ;
#10291=PRODUCT ( '8. Upper Jaw Support', '8. Upper Jaw Support', '', ( #44206 ) ) ;
#10319=DIRECTION ( 'NONE',  ( 0.000000000000000000, -0.000000000000000000, 1.000000000000000000 ) ) ;
#10327=FACE_OUTER_BOUND ( 'NONE', #40065, .T. ) ;
#10353=FACE_OUTER_BOUND ( 'NONE', #50755, .T. ) ;
#10373=ORIENTED_EDGE ( 'NONE', *, *, #807, .T. ) ;
#10380=CARTESIAN_POINT ( 'NONE',  ( 0.000000000000000000, -3.500000000000000000, 24.00000000000000000 ) ) ;
#10392=PLANE ( 'NONE',  #13388 ) ;
#10414=VECTOR ( 'NONE', #44610, 1000.000000000000000 ) ;
#10418=ORIENTED_EDGE ( 'NONE', *, *, #20652, .T. ) ;
#10466=ORIENTED_EDGE ( 'NONE', *, *, #28648, .T. ) ;
#10490=CARTESIAN_POINT ( 'NONE',  ( -11.74999999999999645, -3.000000000000000000, 6.000000000000001776 ) ) ;
#10500=CARTESIAN_POINT ( 'NONE',  ( -54.93556801395976663, -8.762778093175660032, -2.499999999999992895 ) ) ;
#10539=ORIENTED_EDGE ( 'NONE', *, *, #29145, .T. ) ;
#10541=CARTESIAN_POINT ( 'NONE',  ( 3.129636159629258261E-31, -7.500000000000000888, 23.00000000000000000 ) ) ;
#10551=DIRECTION ( 'NONE',  ( -0.4834014344020922671, 0.000000000000000000, 0.8753987966738359106 ) ) ;
#10559=PLANE ( 'NONE',  #59231 ) ;
#10639=CARTESIAN_POINT ( 'NONE',  ( -70.75000000000000000, -0.9999999999999995559, 20.00000000000000000 ) ) ;
#10663=CARTESIAN_POINT ( 'NONE',  ( -55.78467112892083435, -8.499999999999994671, 5.997393757699851058 ) ) ;
#10674=VERTEX_POINT ( 'NONE', #47733 ) ;
#10675=ADVANCED_FACE ( 'NONE', ( #14989 ), #10392, .T. ) ;
#10677=SURFACE_STYLE_USAGE ( .BOTH. , #20889 ) ;
#10683=LINE ( 'NONE', #27521, #47096 ) ;
#10703=ORIENTED_EDGE ( 'NONE', *, *, #3718, .T. ) ;
#10719=ADVANCED_FACE ( 'NONE', ( #10039 ), #48279, .F. ) ;
#10776=DIRECTION ( 'NONE',  ( 0.000000000000000000, 0.000000000000000000, -1.000000000000000000 ) ) ;
#10807=DIRECTION ( 'NONE',  ( 1.000000000000000000, -1.445602896647339656E-16, -0.000000000000000000 ) ) ;
#10812=CARTESIAN_POINT ( 'NONE',  ( 1.189524669241243060E-16, -7.500000000000000888, 24.00000000000000000 ) ) ;
#10824=DIRECTION ( 'NONE',  ( 1.000000000000000000, 0.000000000000000000, 0.000000000000000000 ) ) ;
#10826=VERTEX_POINT ( 'NONE', #52950 ) ;
#10903=ADVANCED_FACE ( 'NONE', ( #24044 ), #12586, .T. ) ;
#10941=FACE_OUTER_BOUND ( 'NONE', #22499, .T. ) ;
#10947=ORIENTED_EDGE ( 'NONE', *, *, #34966, .T. ) ;
#11006=EDGE_CURVE ( 'NONE', #10674, #26634, #6003, .T. ) ;
#11013=DIRECTION ( 'NONE',  ( -0.000000000000000000, 1.000000000000000000, -0.000000000000000000 ) ) ;
#11072=CARTESIAN_POINT ( 'NONE',  ( -7.731910350068054619E-16, -6.500000000000000888, 3.000000000000000000 ) ) ;
#11080=( GEOMETRIC_REPRESENTATION_CONTEXT ( 3 ) GLOBAL_UNCERTAINTY_ASSIGNED_CONTEXT ( ( #33478 ) ) GLOBAL_UNIT_ASSIGNED_CONTEXT ( ( #68518, #53038, #31199 ) ) REPRESENTATION_CONTEXT ( 'NONE', 'WORKASPACE' ) );
#11129=EDGE_CURVE ( 'NONE', #20689, #43029, #16226, .T. ) ;
#11150=ORIENTED_EDGE ( 'NONE', *, *, #1842, .T. ) ;
#11166=EDGE_LOOP ( 'NONE', ( #44484, #55461, #5510, #22985, #33559, #41610 ) ) ;
#11174=VECTOR ( 'NONE', #32434, 1000.000000000000000 ) ;
#11268=CARTESIAN_POINT ( 'NONE',  ( -57.11974195712093660, -13.49999999999999112, -2.000000000000000000 ) ) ;
#11274=EDGE_CURVE ( 'NONE', #29573, #65886, #6642, .T. ) ;
#11280=VECTOR ( 'NONE', #20789, 1000.000000000000000 ) ;
#11305=PRODUCT_DEFINITION_FORMATION_WITH_SPECIFIED_SOURCE ( 'ANY', '', #10291, .NOT_KNOWN. ) ;
#11318=CYLINDRICAL_SURFACE ( 'NONE', #21630, 1.000000000000000888 ) ;
#11320=CARTESIAN_POINT ( 'NONE',  ( -33.58491031241940306, -9.466447511860014430, -3.170070218111009197 ) ) ;
#11351=CARTESIAN_POINT ( 'NONE',  ( -7.731910350068054619E-16, -6.500000000000000888, 3.000000000000000000 ) ) ;
#11360=FACE_OUTER_BOUND ( 'NONE', #65371, .T. ) ;
#11410=DIRECTION ( 'NONE',  ( 0.000000000000000000, -0.000000000000000000, 1.000000000000000000 ) ) ;
#11457=PLANE ( 'NONE',  #20372 ) ;
#11459=DIRECTION ( 'NONE',  ( 1.000000000000000000, 0.000000000000000000, 0.000000000000000000 ) ) ;
#11480=EDGE_CURVE ( 'NONE', #20740, #17716, #28209, .T. ) ;
#11481=VECTOR ( 'NONE', #17892, 1000.000000000000000 ) ;
#11488=DIRECTION ( 'NONE',  ( -1.000000000000000000, 1.189524669241239115E-16, 0.000000000000000000 ) ) ;
#11502=VECTOR ( 'NONE', #42360, 1000.000000000000000 ) ;
#11515=ORIENTED_EDGE ( 'NONE', *, *, #37637, .T. ) ;
#11649=CARTESIAN_POINT ( 'NONE',  ( -55.74597125125978181, -8.678695864509879954, -1.659950873073223976 ) ) ;
#11692=AXIS2_PLACEMENT_3D ( 'NONE', #26057, #60477, #43349 ) ;
#11713=CARTESIAN_POINT ( 'NONE',  ( -47.54356174116917089, -13.47739874223435130, 2.712348457220836728 ) ) ;
#11731=FACE_OUTER_BOUND ( 'NONE', #43767, .T. ) ;
#11743=LINE ( 'NONE', #33548, #58681 ) ;
#11781=LINE ( 'NONE', #28266, #34203 ) ;
#11806=ORIENTED_EDGE ( 'NONE', *, *, #49656, .F. ) ;
#11815=DIRECTION ( 'NONE',  ( -0.000000000000000000, 0.000000000000000000, -1.000000000000000000 ) ) ;
#11830=VERTEX_POINT ( 'NONE', #63437 ) ;
#11849=ADVANCED_FACE ( 'NONE', ( #10327 ), #27834, .T. ) ;
#11864=AXIS2_PLACEMENT_3D ( 'NONE', #13936, #57183, #56855 ) ;
#11871=FACE_OUTER_BOUND ( 'NONE', #39442, .T. ) ;
#11895=CARTESIAN_POINT ( 'NONE',  ( -53.18756747357285519, -10.02680648607945102, -3.500000000000002220 ) ) ;
#11925=DIRECTION ( 'NONE',  ( 0.000000000000000000, 0.000000000000000000, -1.000000000000000000 ) ) ;
#11947=ORIENTED_EDGE ( 'NONE', *, *, #53258, .T. ) ;
#11975=DIRECTION ( 'NONE',  ( 0.000000000000000000, 0.000000000000000000, -1.000000000000000000 ) ) ;
#11978=CARTESIAN_POINT ( 'NONE',  ( -47.48752445902327679, -11.75819929757497206, 3.312120501307041387 ) ) ;
#11982=CARTESIAN_POINT ( 'NONE',  ( -7.731910350068054619E-16, -6.500000000000000888, 21.00000000000000000 ) ) ;
#11986=VERTEX_POINT ( 'NONE', #6405 ) ;
#11993=FACE_OUTER_BOUND ( 'NONE', #46474, .T. ) ;
#12000=EDGE_CURVE ( 'NONE', #33368, #20590, #58855, .T. ) ;
#12018=ORIENTED_EDGE ( 'NONE', *, *, #54012, .F. ) ;
#12030=DIRECTION ( 'NONE',  ( 0.9604119879385738523, 0.2638002197014291950, 0.08954472351487077764 ) ) ;
#12043=CIRCLE ( 'NONE', #65976, 3.100000000000003642 ) ;
#12044=FACE_OUTER_BOUND ( 'NONE', #22476, .T. ) ;
#12045=CARTESIAN_POINT ( 'NONE',  ( -45.98142172590127075, -12.02919239290969955, 3.220909842096380871 ) ) ;
#12106=CARTESIAN_POINT ( 'NONE',  ( -53.78456796010189578, -9.630272325962776492, -3.117062346851436683 ) ) ;
#12111=SPHERICAL_SURFACE ( 'NONE', #45978, 1.000000000000000000 ) ;
#12122=CARTESIAN_POINT ( 'NONE',  ( -74.75000000000000000, -3.000000000000000000, 7.000000000000001776 ) ) ;
#12138=LINE ( 'NONE', #59991, #27080 ) ;
#12142=DIRECTION ( 'NONE',  ( -1.000000000000000000, 1.445602896647339656E-16, -0.000000000000000000 ) ) ;
#12152=PLANE ( 'NONE',  #47371 ) ;
#12163=VECTOR ( 'NONE', #18702, 1000.000000000000000 ) ;
#12195=CARTESIAN_POINT ( 'NONE',  ( -37.66801306575244013, -11.00887909414482380, 3.663666223797411803 ) ) ;
#12232=ORIENTED_EDGE ( 'NONE', *, *, #41423, .T. ) ;
#12279=CARTESIAN_POINT ( 'NONE',  ( -26.79538245034556709, -8.499999999999998224, 0.000000000000000000 ) ) ;
#12318=CARTESIAN_POINT ( 'NONE',  ( -55.36563020516651790, -8.495980172839733058, -2.204722216948698854 ) ) ;
#12322=ORIENTED_EDGE ( 'NONE', *, *, #31912, .F. ) ;
#12340=CARTESIAN_POINT ( 'NONE',  ( -32.80478667408987548, -9.106085870130632642, -2.687031549326329039 ) ) ;
#12349=DIRECTION ( 'NONE',  ( -0.000000000000000000, -0.000000000000000000, 1.000000000000000000 ) ) ;
#12350=DIRECTION ( 'NONE',  ( 1.000000000000000000, 0.000000000000000000, -0.000000000000000000 ) ) ;
#12381=CARTESIAN_POINT ( 'NONE',  ( -70.75000000000000000, -0.9999999999999995559, 24.00000000000000000 ) ) ;
#12384=CARTESIAN_POINT ( 'NONE',  ( -40.79052781025667684, -13.69784301587829667, 2.689112900518555005 ) ) ;
#12397=DIRECTION ( 'NONE',  ( 0.000000000000000000, 0.000000000000000000, -1.000000000000000000 ) ) ;
#12428=CARTESIAN_POINT ( 'NONE',  ( -51.25481733270894580, -11.82219366972335095, 1.525841347188607422 ) ) ;
#12431=STYLED_ITEM ( 'NONE', ( #21583 ), #52368 ) ;
#12446=DIRECTION ( 'NONE',  ( -0.000000000000000000, 0.000000000000000000, -1.000000000000000000 ) ) ;
#12450=CYLINDRICAL_SURFACE ( 'NONE', #27278, 1.000000000000000888 ) ;
#12469=EDGE_CURVE ( 'NONE', #34584, #58716, #707, .T. ) ;
#12478=CARTESIAN_POINT ( 'NONE',  ( -48.29019130588075370, -13.25700720320236847, 0.9673485149590689280 ) ) ;
#12497=FACE_OUTER_BOUND ( 'NONE', #60457, .T. ) ;
#12529=ORIENTED_EDGE ( 'NONE', *, *, #27850, .T. ) ;
#12586=( BOUNDED_SURFACE ( )  B_SPLINE_SURFACE ( 3, 2, ( 
 ( #50783, #44846, #40242 ),
 ( #60613, #50105, #34946 ),
 ( #61321, #7180, #55710 ),
 ( #39213, #45548, #13132 ),
 ( #56391, #18077, #39564 ),
 ( #45193, #60967, #28942 ),
 ( #12428, #2534, #66970 ),
 ( #18431, #2161, #23693 ),
 ( #50434, #18765, #66616 ),
 ( #33889, #66250, #55357 ),
 ( #28608, #1834, #11978 ),
 ( #44730, #322, #55224 ) ),
 .UNSPECIFIED., .F., .F., .F. ) 
 B_SPLINE_SURFACE_WITH_KNOTS ( ( 4, 2, 2, 2, 2, 4 ),
 ( 3, 3 ),
 ( 8.673617379884035472E-19, 0.001495124371074673829, 0.002242686556612010201, 0.002990248742149346790, 0.004485373113224019534, 0.005980497484298692712 ),
 ( 0.000000000000000000, 1.000000000000000000 ),
 .UNSPECIFIED. ) 
 GEOMETRIC_REPRESENTATION_ITEM ( )  RATIONAL_B_SPLINE_SURFACE ( (
 ( 1.000000000000000000, 0.8674236696762898102, 1.000000000000000000),
 ( 1.000000000000000000, 0.8646670541289291911, 1.000000000000000000),
 ( 1.000000000000000000, 0.8610282887621616421, 1.000000000000000000),
 ( 1.000000000000000000, 0.8545310245463959564, 1.000000000000000000),
 ( 1.000000000000000000, 0.8521934417079706225, 1.000000000000000000),
 ( 1.000000000000000000, 0.8472483593196091789, 1.000000000000000000),
 ( 1.000000000000000000, 0.8446295995112632626, 1.000000000000000000),
 ( 1.000000000000000000, 0.8366484175561841319, 1.000000000000000000),
 ( 1.000000000000000000, 0.8311340418845757361, 1.000000000000000000),
 ( 1.000000000000000000, 0.8205640772812347050, 1.000000000000000000),
 ( 1.000000000000000000, 0.8154939450290221714, 1.000000000000000000),
 ( 1.000000000000000000, 0.8111477107414829524, 1.000000000000000000) ) ) 
 REPRESENTATION_ITEM ( '' )  SURFACE ( )  );
#12607=CARTESIAN_POINT ( 'NONE',  ( -30.38025804287905629, -13.49999999999999822, -7.000000000000000000 ) ) ;
#12660=ORIENTED_EDGE ( 'NONE', *, *, #28394, .T. ) ;
#12697=CARTESIAN_POINT ( 'NONE',  ( -32.56443198605217049, -8.762778093183483108, -2.500000000007921219 ) ) ;
#12740=DIRECTION ( 'NONE',  ( -1.000000000000000000, 0.000000000000000000, 0.000000000000000000 ) ) ;
#12777=AXIS2_PLACEMENT_3D ( 'NONE', #46323, #46689, #9715 ) ;
#12788=CARTESIAN_POINT ( 'NONE',  ( -83.49999999999998579, 4.336808689942018722E-16, 24.00000000000000000 ) ) ;
#12800=CARTESIAN_POINT ( 'NONE',  ( -52.74999999999999289, 0.000000000000000000, -2.000000000000000000 ) ) ;
#12807=LINE ( 'NONE', #19471, #9964 ) ;
#12818=CARTESIAN_POINT ( 'NONE',  ( -35.65778776279520912, -9.947368421052624754, 4.481646853389230856 ) ) ;
#12819=EDGE_LOOP ( 'NONE', ( #58699, #53405, #23789, #64622 ) ) ;
#12834=CARTESIAN_POINT ( 'NONE',  ( -51.93475478252885580, -11.36189310745057846, 1.762106798099256411 ) ) ;
#12835=CARTESIAN_POINT ( 'NONE',  ( -52.74999999999999289, 0.000000000000000000, -7.000000000000000000 ) ) ;
#12860=EDGE_CURVE ( 'NONE', #43417, #17125, #39249, .T. ) ;
#12886=CARTESIAN_POINT ( 'NONE',  ( -43.75000000000000000, 4.336808689942018722E-16, 0.000000000000000000 ) ) ;
#12905=CARTESIAN_POINT ( 'NONE',  ( -35.20898490747966747, -11.12536675346265724, 3.476728976952998096 ) ) ;
#12912=B_SPLINE_CURVE_WITH_KNOTS ( 'NONE', 3,
 ( #38019, #1676, #23195, #32689, #54143, #64718, #16559, #59407, #2349, #8737 ),
 .UNSPECIFIED., .F., .F.,
 ( 4, 2, 2, 2, 4 ),
 ( 0.000000000000000000, 0.001951620466334530717, 0.003903240932669061435, 0.005854861399003591718, 0.007806481865338122869 ),
 .UNSPECIFIED. ) ;
#13051=ORIENTED_EDGE ( 'NONE', *, *, #22813, .T. ) ;
#13056=VERTEX_POINT ( 'NONE', #60649 ) ;
#13111=EDGE_LOOP ( 'NONE', ( #15981, #61134, #35450, #18908 ) ) ;
#13126=VERTEX_POINT ( 'NONE', #36418 ) ;
#13132=CARTESIAN_POINT ( 'NONE',  ( -50.68995449411814036, -10.61513085179375970, 3.914528793814394891 ) ) ;
#13178=DIRECTION ( 'NONE',  ( 1.000000000000000000, 1.084202172485503448E-16, 0.000000000000000000 ) ) ;
#13183=CARTESIAN_POINT ( 'NONE',  ( -57.58629378005873889, -7.761720733523185700, -0.7755720678490086728 ) ) ;
#13277=VERTEX_POINT ( 'NONE', #55914 ) ;
#13308=CARTESIAN_POINT ( 'NONE',  ( -32.76851741822089537, -9.107254030097822195, -1.999999999999996225 ) ) ;
#13326=CARTESIAN_POINT ( 'NONE',  ( -26.79538245034556709, -8.499999999999996447, 1.000000000000000000 ) ) ;
#13350=ORIENTED_EDGE ( 'NONE', *, *, #67041, .F. ) ;
#13367=ORIENTED_EDGE ( 'NONE', *, *, #38841, .T. ) ;
#13380=AXIS2_PLACEMENT_3D ( 'NONE', #61744, #49851, #8326 ) ;
#13388=AXIS2_PLACEMENT_3D ( 'NONE', #4033, #4365, #47014 ) ;
#13406=EDGE_CURVE ( 'NONE', #19259, #30231, #33760, .T. ) ;
#13414=DIRECTION ( 'NONE',  ( 0.000000000000000000, 0.000000000000000000, -1.000000000000000000 ) ) ;
#13506=ADVANCED_FACE ( 'NONE', ( #36228 ), #8440, .F. ) ;
#13552=CARTESIAN_POINT ( 'NONE',  ( -30.38025804287905629, -8.499999999999996447, 8.000000000000000000 ) ) ;
#13568=EDGE_CURVE ( 'NONE', #33368, #51912, #49548, .T. ) ;
#13603=CARTESIAN_POINT ( 'NONE',  ( -58.75000000000000000, -13.99999999999999822, 15.00000000000000178 ) ) ;
#13604=DIRECTION ( 'NONE',  ( 0.000000000000000000, 0.000000000000000000, -1.000000000000000000 ) ) ;
#13605=MECHANICAL_DESIGN_GEOMETRIC_PRESENTATION_REPRESENTATION('',(#20346),#47360);
#13607=AXIS2_PLACEMENT_3D ( 'NONE', #3140, #13758, #20418 ) ;
#13641=CARTESIAN_POINT ( 'NONE',  ( -54.73909702325379101, -9.103123100731311368, -2.346905346906726031 ) ) ;
#13650=CARTESIAN_POINT ( 'NONE',  ( 3.851859888774471706E-31, -7.500000000000000888, 1.000000000000000000 ) ) ;
#13678=CARTESIAN_POINT ( 'NONE',  ( -3.000000000000000000, -2.499999999999999556, 0.000000000000000000 ) ) ;
#13715=AXIS2_PLACEMENT_3D ( 'NONE', #15948, #37774, #59154 ) ;
#13743=EDGE_CURVE ( 'NONE', #54598, #26367, #18115, .T. ) ;
#13748=DIRECTION ( 'NONE',  ( 1.000000000000000000, 0.000000000000000000, 0.000000000000000000 ) ) ;
#13758=DIRECTION ( 'NONE',  ( 0.000000000000000000, -1.000000000000000000, -0.000000000000000000 ) ) ;
#13783=VECTOR ( 'NONE', #12142, 1000.000000000000000 ) ;
#13829=ORIENTED_EDGE ( 'NONE', *, *, #11274, .T. ) ;
#13885=SURFACE_SIDE_STYLE ('',( #45917 ) ) ;
#13936=CARTESIAN_POINT ( 'NONE',  ( -57.11974195712093660, -13.49999999999999467, -7.000000000000000000 ) ) ;
#13943=CARTESIAN_POINT ( 'NONE',  ( -60.70461754965443646, -7.499999999999992006, 0.000000000000000000 ) ) ;
#13975=EDGE_CURVE ( 'NONE', #33970, #51601, #7632, .T. ) ;
#13992=CARTESIAN_POINT ( 'NONE',  ( -71.75000000000000000, -3.000000000000000000, 20.00000000000000000 ) ) ;
#14019=CARTESIAN_POINT ( 'NONE',  ( -40.04190075645215785, -13.49999999999999822, 0.8979962945199000401 ) ) ;
#14023=CARTESIAN_POINT ( 'NONE',  ( -31.53475076290974499, -8.620751121487828073, -1.503968433715946240 ) ) ;
#14055=ORIENTED_EDGE ( 'NONE', *, *, #13975, .F. ) ;
#14066=ORIENTED_EDGE ( 'NONE', *, *, #39521, .F. ) ;
#14084=EDGE_CURVE ( 'NONE', #13277, #24594, #42684, .T. ) ;
#14108=CARTESIAN_POINT ( 'NONE',  ( -60.70461754965443646, -7.499999999999993783, 1.000000000000000000 ) ) ;
#14115=CARTESIAN_POINT ( 'NONE',  ( -57.11974195712091529, -8.499999999999996447, 7.999999999999976019 ) ) ;
#14117=ORIENTED_EDGE ( 'NONE', *, *, #13975, .T. ) ;
#14133=CARTESIAN_POINT ( 'NONE',  ( -34.31243252642735087, -10.02680648607962510, -3.499999999999997335 ) ) ;
#14147=ADVANCED_FACE ( 'NONE', ( #50146 ), #6495, .T. ) ;
#14151=DIRECTION ( 'NONE',  ( 1.000000000000000000, 0.000000000000000000, 0.000000000000000000 ) ) ;
#14161=CARTESIAN_POINT ( 'NONE',  ( -71.75000000000000000, -0.9999999999999995559, 20.00000000000000000 ) ) ;
#14256=CARTESIAN_POINT ( 'NONE',  ( -30.38025804287905629, -8.499999999999996447, 8.000000000000000000 ) ) ;
#14317=VERTEX_POINT ( 'NONE', #25123 ) ;
#14381=EDGE_CURVE ( 'NONE', #24594, #34584, #47682, .T. ) ;
#14452=CARTESIAN_POINT ( 'NONE',  ( -74.75000000000000000, -0.9999999999999995559, 7.000000000000001776 ) ) ;
#14463=EDGE_CURVE ( 'NONE', #22460, #54909, #3992, .T. ) ;
#14468=ORIENTED_EDGE ( 'NONE', *, *, #52842, .T. ) ;
#14523=VERTEX_POINT ( 'NONE', #14943 ) ;
#14530=EDGE_CURVE ( 'NONE', #20740, #57439, #10683, .T. ) ;
#14542=B_SPLINE_CURVE_WITH_KNOTS ( 'NONE', 3,
 ( #4940, #32021, #65420, #21117, #6315, #26717, #15871, #53147 ),
 .UNSPECIFIED., .F., .F.,
 ( 4, 2, 2, 4 ),
 ( 1.425583368063878336E-15, 0.0009391389479451172110, 0.001878277895888808696, 0.003756555791776202725 ),
 .UNSPECIFIED. ) ;
#14579=FACE_OUTER_BOUND ( 'NONE', #22841, .T. ) ;
#14624=CYLINDRICAL_SURFACE ( 'NONE', #53278, 1.000000000000000888 ) ;
#14646=DIRECTION ( 'NONE',  ( -1.000000000000000000, 0.000000000000000000, 0.000000000000000000 ) ) ;
#14720=CARTESIAN_POINT ( 'NONE',  ( -75.50000000000000000, -8.499999999999991118, 21.00000000000000000 ) ) ;
#14722=CARTESIAN_POINT ( 'NONE',  ( -35.25000000000000000, 4.336808689942018722E-16, -5.099999999999999645 ) ) ;
#14784=CIRCLE ( 'NONE', #25949, 1.000000000000000000 ) ;
#14815=DIRECTION ( 'NONE',  ( -1.000000000000000000, 0.000000000000000000, -0.000000000000000000 ) ) ;
#14821=AXIS2_PLACEMENT_3D ( 'NONE', #39934, #55728, #26961 ) ;
#14822=ADVANCED_FACE ( 'NONE', ( #23715 ), #12111, .T. ) ;
#14871=LINE ( 'NONE', #25738, #49543 ) ;
#14916=DIRECTION ( 'NONE',  ( 0.000000000000000000, 0.000000000000000000, 1.000000000000000000 ) ) ;
#14934=ORIENTED_EDGE ( 'NONE', *, *, #27307, .F. ) ;
#14943=CARTESIAN_POINT ( 'NONE',  ( -1.011095968855053334E-15, -8.500000000000000000, 3.000000000000000000 ) ) ;
#14950=SURFACE_STYLE_USAGE ( .BOTH. , #31087 ) ;
#14971=CARTESIAN_POINT ( 'NONE',  ( -34.28383209646202801, -10.32887243014199363, 2.406038820785245225 ) ) ;
#14986=VECTOR ( 'NONE', #52069, 1000.000000000000000 ) ;
#14989=FACE_OUTER_BOUND ( 'NONE', #47079, .T. ) ;
#15013=AXIS2_PLACEMENT_3D ( 'NONE', #5554, #36616, #48533 ) ;
#15085=CARTESIAN_POINT ( 'NONE',  ( -33.89861118948982721, -9.947368421052631859, 2.722470280083840066 ) ) ;
#15112=CARTESIAN_POINT ( 'NONE',  ( -38.44653593450800599, -11.31074412437664378, 3.500884832118608792 ) ) ;
#15132=ADVANCED_FACE ( 'NONE', ( #33166 ), #60551, .F. ) ;
#15145=ORIENTED_EDGE ( 'NONE', *, *, #59538, .T. ) ;
#15185=CARTESIAN_POINT ( 'NONE',  ( -11.99999999999999822, -6.499999999999999112, 21.00000000000000000 ) ) ;
#15186=FACE_OUTER_BOUND ( 'NONE', #5347, .T. ) ;
#15195=ORIENTED_EDGE ( 'NONE', *, *, #54223, .T. ) ;
#15197=AXIS2_PLACEMENT_3D ( 'NONE', #5076, #32486, #64527 ) ;
#15202=CARTESIAN_POINT ( 'NONE',  ( -75.75000000000000000, -3.000000000000000000, 6.000000000000001776 ) ) ;
#15203=CIRCLE ( 'NONE', #67956, 1.000000000000000888 ) ;
#15218=LINE ( 'NONE', #42317, #25366 ) ;
#15230=DIRECTION ( 'NONE',  ( 1.000000000000000000, -1.084202172485504434E-16, -0.000000000000000000 ) ) ;
#15300=FILL_AREA_STYLE_COLOUR ( '', #19218 ) ;
#15331=ORIENTED_EDGE ( 'NONE', *, *, #21342, .F. ) ;
#15336=CARTESIAN_POINT ( 'NONE',  ( -58.57094193006191318, -7.669019089512441489, -0.3330098372451437139 ) ) ;
#15427=CARTESIAN_POINT ( 'NONE',  ( -34.48878133304234694, -10.53184416402257284, 3.891476709836706238 ) ) ;
#15431=DIRECTION ( 'NONE',  ( 1.000000000000000000, 0.000000000000000000, 0.000000000000000000 ) ) ;
#15473=ORIENTED_EDGE ( 'NONE', *, *, #35689, .F. ) ;
#15531=CARTESIAN_POINT ( 'NONE',  ( -15.75000000000000000, -3.000000000000000000, 20.00000000000000000 ) ) ;
#15557=EDGE_LOOP ( 'NONE', ( #15473, #51617, #14468, #47987 ) ) ;
#15614=CARTESIAN_POINT ( 'NONE',  ( -37.75000000000000000, 0.000000000000000000, -6.999999999999999112 ) ) ;
#15639=SURFACE_STYLE_FILL_AREA ( #46984 ) ;
#15645=ORIENTED_EDGE ( 'NONE', *, *, #24463, .T. ) ;
#15657=CARTESIAN_POINT ( 'NONE',  ( -39.44036755984751608, -13.33477445990380517, 0.9440656176847447290 ) ) ;
#15719=DIRECTION ( 'NONE',  ( 0.000000000000000000, 0.000000000000000000, -1.000000000000000000 ) ) ;
#15733=DIRECTION ( 'NONE',  ( 0.000000000000000000, -0.000000000000000000, 1.000000000000000000 ) ) ;
#15757=LINE ( 'NONE', #58994, #1482 ) ;
#15871=CARTESIAN_POINT ( 'NONE',  ( -27.42392015114097958, -8.499999999999994671, 0.9999999999999991118 ) ) ;
#15906=EDGE_CURVE ( 'NONE', #59113, #14523, #62815, .T. ) ;
#15920=ORIENTED_EDGE ( 'NONE', *, *, #6993, .F. ) ;
#15948=CARTESIAN_POINT ( 'NONE',  ( -15.75000000000000000, -0.9999999999999995559, 20.00000000000000000 ) ) ;
#15979=DIRECTION ( 'NONE',  ( 1.000000000000000000, -1.445602896647339656E-16, 0.000000000000000000 ) ) ;
#15981=ORIENTED_EDGE ( 'NONE', *, *, #30260, .T. ) ;
#15983=PRESENTATION_STYLE_ASSIGNMENT (( #10677 ) ) ;
#15988=VECTOR ( 'NONE', #53359, 1000.000000000000000 ) ;
#15996=EDGE_CURVE ( 'NONE', #23645, #60509, #43082, .T. ) ;
#16012=CARTESIAN_POINT ( 'NONE',  ( -32.39999086766104597, -8.921669375848802375, -1.645138194676287080 ) ) ;
#16018=CARTESIAN_POINT ( 'NONE',  ( -35.39493682010693476, -11.23731683406899329, 1.831091074604741520 ) ) ;
#16066=DIRECTION ( 'NONE',  ( -1.000000000000000000, 3.552713678800500929E-15, 0.000000000000000000 ) ) ;
#16099=ORIENTED_EDGE ( 'NONE', *, *, #56064, .F. ) ;
#16108=DIRECTION ( 'NONE',  ( -0.000000000000000000, -0.000000000000000000, -1.000000000000000000 ) ) ;
#16112=CYLINDRICAL_SURFACE ( 'NONE', #8221, 1.000000000000000000 ) ;
#16136=DIRECTION ( 'NONE',  ( -1.189524669241239115E-16, -1.000000000000000000, -0.000000000000000000 ) ) ;
#16168=ORIENTED_EDGE ( 'NONE', *, *, #33137, .F. ) ;
#16207=DIRECTION ( 'NONE',  ( 0.000000000000000000, 0.000000000000000000, -1.000000000000000000 ) ) ;
#16211=DIRECTION ( 'NONE',  ( -1.000000000000000000, 1.189524669241239115E-16, 0.000000000000000000 ) ) ;
#16216=DIRECTION ( 'NONE',  ( -1.000000000000000000, 1.189524669241239115E-16, 0.000000000000000000 ) ) ;
#16226=LINE ( 'NONE', #10231, #11280 ) ;
#16306=ADVANCED_FACE ( 'NONE', ( #53830 ), #5627, .T. ) ;
#16340=CARTESIAN_POINT ( 'NONE',  ( -46.95366099282699679, -13.64295980804098996, 2.693440547789818673 ) ) ;
#16389=AXIS2_PLACEMENT_3D ( 'NONE', #60109, #6994, #43980 ) ;
#16392=LINE ( 'NONE', #779, #733 ) ;
#16417=CARTESIAN_POINT ( 'NONE',  ( -15.75000000000000000, -0.9999999999999995559, 20.00000000000000000 ) ) ;
#16444=ADVANCED_FACE ( 'NONE', ( #35854 ), #30548, .F. ) ;
#16462=CARTESIAN_POINT ( 'NONE',  ( -43.75000000000000000, 0.000000000000000000, -7.000000000000000000 ) ) ;
#16478=ADVANCED_FACE ( 'NONE', ( #40455 ), #62910, .T. ) ;
#16532=CARTESIAN_POINT ( 'NONE',  ( -15.75000000000000000, -3.000000000000000000, 20.00000000000000000 ) ) ;
#16542=ORIENTED_EDGE ( 'NONE', *, *, #32236, .T. ) ;
#16559=CARTESIAN_POINT ( 'NONE',  ( -45.18758536601421127, -13.94086583230001963, 0.7847372218215835638 ) ) ;
#16610=EDGE_LOOP ( 'NONE', ( #38757, #69594, #67122, #65007 ) ) ;
#16632=CARTESIAN_POINT ( 'NONE',  ( -33.93450318706182856, -9.954220776862968023, -2.519071624164639367 ) ) ;
#16653=( BOUNDED_SURFACE ( )  B_SPLINE_SURFACE ( 3, 2, ( 
 ( #21874, #22915, #5657 ),
 ( #65815, #54555, #60506 ),
 ( #1009, #1383, #12318 ),
 ( #17647, #11649, #64128 ),
 ( #33788, #65464, #7066 ),
 ( #38438, #48280, #17313 ),
 ( #64773, #21507, #32391 ),
 ( #38775, #43025, #33453 ) ),
 .UNSPECIFIED., .F., .F., .F. ) 
 B_SPLINE_SURFACE_WITH_KNOTS ( ( 4, 2, 2, 4 ),
 ( 3, 3 ),
 ( 1.468465106457816916E-14, 0.0009031189008530563856, 0.001806237801691428120, 0.003612475603368171806 ),
 ( 0.000000000000000000, 1.000000000000000000 ),
 .UNSPECIFIED. ) 
 GEOMETRIC_REPRESENTATION_ITEM ( )  RATIONAL_B_SPLINE_SURFACE ( (
 ( 1.000000000000000000, 0.9473232638936814887, 1.000000000000000000),
 ( 1.000000000000000000, 0.9379074176463484402, 1.000000000000000000),
 ( 1.000000000000000000, 0.9271920136555387160, 1.000000000000000000),
 ( 1.000000000000000000, 0.9038526065441394586, 1.000000000000000000),
 ( 1.000000000000000000, 0.8912230047972187208, 1.000000000000000000),
 ( 1.000000000000000000, 0.8514336325998846933, 1.000000000000000000),
 ( 1.000000000000000000, 0.8221224512773489534, 1.000000000000000000),
 ( 1.000000000000000000, 0.7942671885213410388, 1.000000000000000000) ) ) 
 REPRESENTATION_ITEM ( '' )  SURFACE ( )  );
#16656=CARTESIAN_POINT ( 'NONE',  ( -53.60138881051016568, -9.947368421052624754, 2.722470280083841843 ) ) ;
#16699=DIRECTION ( 'NONE',  ( -1.000000000000000000, -0.000000000000000000, -0.000000000000000000 ) ) ;
#16707=CARTESIAN_POINT ( 'NONE',  ( -33.93619543054067123, -9.954544408048933590, -2.527596102671208822 ) ) ;
#16735=ORIENTED_EDGE ( 'NONE', *, *, #32471, .F. ) ;
#16764=DIRECTION ( 'NONE',  ( -1.000000000000000000, 0.000000000000000000, -0.000000000000000000 ) ) ;
#16777=EDGE_LOOP ( 'NONE', ( #54100, #25170, #50530, #931 ) ) ;
#16786=AXIS2_PLACEMENT_3D ( 'NONE', #5089, #26541, #31816 ) ;
#16994=DIRECTION ( 'NONE',  ( 0.000000000000000000, 0.000000000000000000, 1.000000000000000000 ) ) ;
#17003=CARTESIAN_POINT ( 'NONE',  ( -33.73135404569435281, -9.688118915736252390, -3.017821087819916315 ) ) ;
#17012=CARTESIAN_POINT ( 'NONE',  ( -46.49706195760896321, -11.95311037025569867, 3.244122449748929160 ) ) ;
#17098=VECTOR ( 'NONE', #51371, 1000.000000000000000 ) ;
#17099=FACE_OUTER_BOUND ( 'NONE', #17348, .T. ) ;
#17115=CARTESIAN_POINT ( 'NONE',  ( -84.49999999999998579, -3.499999999999999556, 24.00000000000000000 ) ) ;
#17121=VERTEX_POINT ( 'NONE', #12835 ) ;
#17125=VERTEX_POINT ( 'NONE', #25129 ) ;
#17133=VERTEX_POINT ( 'NONE', #18125 ) ;
#17134=ORIENTED_EDGE ( 'NONE', *, *, #60236, .F. ) ;
#17239=DIRECTION ( 'NONE',  ( 0.000000000000000000, 0.000000000000000000, -1.000000000000000000 ) ) ;
#17274=CARTESIAN_POINT ( 'NONE',  ( -43.75000000000000000, 4.336808689942018722E-16, -5.099999999999999645 ) ) ;
#17313=CARTESIAN_POINT ( 'NONE',  ( -56.65976306744538959, -7.924810552015186360, -1.308190166797568166 ) ) ;
#17348=EDGE_LOOP ( 'NONE', ( #22372, #7694, #26595 ) ) ;
#17363=CARTESIAN_POINT ( 'NONE',  ( -32.60021343251996484, -9.015750088255582995, -2.278575939230253589 ) ) ;
#17373=CARTESIAN_POINT ( 'NONE',  ( -44.52084369503066341, -13.99284662042119365, 2.674043755914946363 ) ) ;
#17385=ORIENTED_EDGE ( 'NONE', *, *, #36135, .F. ) ;
#17415=ORIENTED_EDGE ( 'NONE', *, *, #44120, .T. ) ;
#17431=CARTESIAN_POINT ( 'NONE',  ( -54.36101593760355399, -9.269969316126742243, -2.682282536902753645 ) ) ;
#17434=DIRECTION ( 'NONE',  ( 0.000000000000000000, -1.000000000000000000, -0.000000000000000000 ) ) ;
#17458=CARTESIAN_POINT ( 'NONE',  ( -52.16324889301085221, -11.19354186750540059, 1.856282217695744530 ) ) ;
#17478=VERTEX_POINT ( 'NONE', #25629 ) ;
#17519=AXIS2_PLACEMENT_3D ( 'NONE', #41795, #58276, #52339 ) ;
#17528=CARTESIAN_POINT ( 'NONE',  ( -36.04767328987400532, -11.70694734933133141, 3.186424117865112926 ) ) ;
#17548=EDGE_CURVE ( 'NONE', #32528, #22579, #8452, .T. ) ;
#17584=DIRECTION ( 'NONE',  ( 0.000000000000000000, 0.000000000000000000, -1.000000000000000000 ) ) ;
#17589=ORIENTED_EDGE ( 'NONE', *, *, #46893, .F. ) ;
#17610=CARTESIAN_POINT ( 'NONE',  ( -58.24585058663792125, -8.499999999999992895, 0.6021708687696052387 ) ) ;
#17647=CARTESIAN_POINT ( 'NONE',  ( -55.47384865756040284, -8.774376589852767694, -1.283477359179545862 ) ) ;
#17665=EDGE_LOOP ( 'NONE', ( #25692, #8835, #52937, #25547 ) ) ;
#17695=LINE ( 'NONE', #2475, #63990 ) ;
#17714=VERTEX_POINT ( 'NONE', #28801 ) ;
#17716=VERTEX_POINT ( 'NONE', #50283 ) ;
#17717=CARTESIAN_POINT ( 'NONE',  ( -74.75000000000000000, -3.000000000000000000, 7.000000000000001776 ) ) ;
#17738=ORIENTED_EDGE ( 'NONE', *, *, #36755, .T. ) ;
#17762=CARTESIAN_POINT ( 'NONE',  ( -71.75000000000000000, -0.9999999999999995559, 19.00000000000000000 ) ) ;
#17797=ORIENTED_EDGE ( 'NONE', *, *, #7814, .T. ) ;
#17818=CARTESIAN_POINT ( 'NONE',  ( -54.93556801395976663, -8.762778093175660032, -2.499999999999992895 ) ) ;
#17873=EDGE_CURVE ( 'NONE', #31107, #24916, #14784, .T. ) ;
#17892=DIRECTION ( 'NONE',  ( 0.000000000000000000, -0.000000000000000000, 1.000000000000000000 ) ) ;
#17908=DIRECTION ( 'NONE',  ( -0.000000000000000000, -0.000000000000000000, -1.000000000000000000 ) ) ;
#17991=ORIENTED_EDGE ( 'NONE', *, *, #57470, .T. ) ;
#17999=CARTESIAN_POINT ( 'NONE',  ( -87.50000000000000000, -8.499999999999989342, 2.999999999999999112 ) ) ;
#18033=AXIS2_PLACEMENT_3D ( 'NONE', #41500, #52404, #56959 ) ;
#18064=CARTESIAN_POINT ( 'NONE',  ( -83.49999999999998579, -2.499999999999999556, 24.00000000000000000 ) ) ;
#18075=DIRECTION ( 'NONE',  ( 0.000000000000000000, -1.000000000000000000, 0.000000000000000000 ) ) ;
#18077=CARTESIAN_POINT ( 'NONE',  ( -51.51464445532459990, -11.66590569038438829, 3.204935539835279901 ) ) ;
#18101=CARTESIAN_POINT ( 'NONE',  ( -7.731910350068054619E-16, -6.500000000000000888, 21.00000000000000000 ) ) ;
#18115=CIRCLE ( 'NONE', #68638, 2.499999999999998224 ) ;
#18125=CARTESIAN_POINT ( 'NONE',  ( -62.28939201416945082, 4.336808689942018722E-16, 0.000000000000000000 ) ) ;
#18126=AXIS2_PLACEMENT_3D ( 'NONE', #47776, #10776, #494 ) ;
#18218=ORIENTED_EDGE ( 'NONE', *, *, #52296, .T. ) ;
#18227=DIRECTION ( 'NONE',  ( 0.000000000000000000, 0.000000000000000000, 1.000000000000000000 ) ) ;
#18232=CARTESIAN_POINT ( 'NONE',  ( -15.75000000000000000, -4.000000000000000000, 20.00000000000000000 ) ) ;
#18245=DIRECTION ( 'NONE',  ( 0.000000000000000000, 0.000000000000000000, 1.000000000000000000 ) ) ;
#18259=CARTESIAN_POINT ( 'NONE',  ( -32.60021343250990356, -9.015750088250115368, -2.278575939223535407 ) ) ;
#18298=EDGE_CURVE ( 'NONE', #19782, #53539, #3958, .T. ) ;
#18307=ORIENTED_EDGE ( 'NONE', *, *, #7449, .T. ) ;
#18317=ORIENTED_EDGE ( 'NONE', *, *, #63399, .T. ) ;
#18340=LINE ( 'NONE', #7081, #61358 ) ;
#18363=ORIENTED_EDGE ( 'NONE', *, *, #702, .F. ) ;
#18372=EDGE_LOOP ( 'NONE', ( #47195, #44774, #51521, #49585 ) ) ;
#18404=DIRECTION ( 'NONE',  ( 0.000000000000000000, 1.000000000000000000, 0.000000000000000000 ) ) ;
#18431=CARTESIAN_POINT ( 'NONE',  ( -50.49993558012277362, -12.27943627009380201, 1.315570835516365777 ) ) ;
#18563=DIRECTION ( 'NONE',  ( 1.000000000000000000, -1.445602896647339656E-16, 0.000000000000000000 ) ) ;
#18574=VERTEX_POINT ( 'NONE', #58077 ) ;
#18578=ORIENTED_EDGE ( 'NONE', *, *, #27388, .F. ) ;
#18594=CARTESIAN_POINT ( 'NONE',  ( -54.23019297999671551, -9.137952730704812510, -3.992206423876322852 ) ) ;
#18618=CARTESIAN_POINT ( 'NONE',  ( -30.43796409298414574, -8.467951584774601415, -0.8043461282435629967 ) ) ;
#18633=CARTESIAN_POINT ( 'NONE',  ( -27.86759363617253271, -7.579901266040472763, -0.06752590370637777395 ) ) ;
#18639=FACE_OUTER_BOUND ( 'NONE', #58589, .T. ) ;
#18658=DIRECTION ( 'NONE',  ( 0.000000000000000000, 0.000000000000000000, -1.000000000000000000 ) ) ;
#18660=EDGE_LOOP ( 'NONE', ( #48393, #32256, #47596, #52051 ) ) ;
#18690=CARTESIAN_POINT ( 'NONE',  ( -49.75000000000000000, 0.000000000000000000, -7.000000000000000000 ) ) ;
#18702=DIRECTION ( 'NONE',  ( 0.000000000000000000, 0.000000000000000000, -1.000000000000000000 ) ) ;
#18710=ORIENTED_EDGE ( 'NONE', *, *, #38841, .F. ) ;
#18715=DIRECTION ( 'NONE',  ( 0.000000000000000000, -1.000000000000000000, -0.000000000000000000 ) ) ;
#18764=ORIENTED_EDGE ( 'NONE', *, *, #13406, .F. ) ;
#18765=CARTESIAN_POINT ( 'NONE',  ( -49.66358509493214513, -12.70625710064021874, 2.845334328481897046 ) ) ;
#18813=VERTEX_POINT ( 'NONE', #64372 ) ;
#18830=CARTESIAN_POINT ( 'NONE',  ( -74.75000000000000000, 4.336808689942018722E-16, 5.000000000000001776 ) ) ;
#18842=FACE_OUTER_BOUND ( 'NONE', #15557, .T. ) ;
#18877=ORIENTED_EDGE ( 'NONE', *, *, #8838, .F. ) ;
#18896=COLOUR_RGB ( '', 0.08235294, 0.09019608, 0.10196078) ;
#18908=ORIENTED_EDGE ( 'NONE', *, *, #62361, .F. ) ;
#18949=DIRECTION ( 'NONE',  ( 0.000000000000000000, -0.000000000000000000, 1.000000000000000000 ) ) ;
#19008=CARTESIAN_POINT ( 'NONE',  ( -57.11974195712091529, -8.499999999999996447, 7.999999999999981348 ) ) ;
#19015=CARTESIAN_POINT ( 'NONE',  ( -44.91955507865309727, -12.15949886118714396, 3.183039689081057944 ) ) ;
#19029=EDGE_CURVE ( 'NONE', #10674, #29467, #2692, .T. ) ;
#19063=B_SPLINE_CURVE_WITH_KNOTS ( 'NONE', 3,
 ( #68653, #63007, #25377, #57750, #63363, #42640 ),
 .UNSPECIFIED., .F., .F.,
 ( 4, 2, 4 ),
 ( -1.190210691535116941E-05, 0.001159215856766632581, 0.002330333820448616568 ),
 .UNSPECIFIED. ) ;
#19134=AXIS2_PLACEMENT_3D ( 'NONE', #58652, #7190, #56613 ) ;
#19138=CARTESIAN_POINT ( 'NONE',  ( -53.60138881051016568, -9.947368421052624754, -2.000000000000000000 ) ) ;
#19142=( BOUNDED_SURFACE ( )  B_SPLINE_SURFACE ( 3, 2, ( 
 ( #13326, #12279, #39076 ),
 ( #2743, #61181, #60471 ),
 ( #23538, #50981, #18633 ),
 ( #66458, #8429, #8064 ),
 ( #28810, #55560, #23892 ),
 ( #29517, #24238, #39766 ) ),
 .UNSPECIFIED., .F., .F., .F. ) 
 B_SPLINE_SURFACE_WITH_KNOTS ( ( 4, 2, 4 ),
 ( 3, 3 ),
 ( 0.000000000000000000, 0.001858233469841190193, 0.003716466939682380385 ),
 ( 0.000000000000000000, 1.000000000000000000 ),
 .UNSPECIFIED. ) 
 GEOMETRIC_REPRESENTATION_ITEM ( )  RATIONAL_B_SPLINE_SURFACE ( (
 ( 1.000000000000000000, 0.7071067811865475727, 1.000000000000000000),
 ( 1.000000000000000000, 0.7208066020895490533, 1.000000000000000000),
 ( 1.000000000000000000, 0.7349590933757870204, 1.000000000000000000),
 ( 1.000000000000000000, 0.7642326935828396284, 1.000000000000000000),
 ( 1.000000000000000000, 0.7794396215065395594, 1.000000000000000000),
 ( 1.000000000000000000, 0.7942671885213410388, 1.000000000000000000) ) ) 
 REPRESENTATION_ITEM ( '' )  SURFACE ( )  );
#19146=ORIENTED_EDGE ( 'NONE', *, *, #25197, .T. ) ;
#19157=CARTESIAN_POINT ( 'NONE',  ( -70.75000000000000000, -4.000000000000000000, 24.00000000000000000 ) ) ;
#19218=COLOUR_RGB ( '', 0.08235294, 0.09019608, 0.10196078) ;
#19245=EDGE_CURVE ( 'NONE', #47861, #1828, #50881, .T. ) ;
#19259=VERTEX_POINT ( 'NONE', #56137 ) ;
#19277=VERTEX_POINT ( 'NONE', #1921 ) ;
#19328=CIRCLE ( 'NONE', #13715, 1.000000000000000888 ) ;
#19336=ORIENTED_EDGE ( 'NONE', *, *, #31765, .T. ) ;
#19370=CARTESIAN_POINT ( 'NONE',  ( -54.62809784357641263, -9.152876382972518599, 4.262533829682994657 ) ) ;
#19409=CARTESIAN_POINT ( 'NONE',  ( -70.75000000000000000, -3.000000000000000000, 24.00000000000000000 ) ) ;
#19432=ORIENTED_EDGE ( 'NONE', *, *, #25487, .F. ) ;
#19445=AXIS2_PLACEMENT_3D ( 'NONE', #21591, #53603, #424 ) ;
#19471=CARTESIAN_POINT ( 'NONE',  ( -57.11974195712093660, -8.499999999999992895, 3.000000000000000000 ) ) ;
#19494=CARTESIAN_POINT ( 'NONE',  ( -53.60138881051015858, -9.947368421052628307, -2.264720458637549338 ) ) ;
#19524=ORIENTED_EDGE ( 'NONE', *, *, #49507, .F. ) ;
#19528=CARTESIAN_POINT ( 'NONE',  ( -35.65778776279520912, -9.947368421052624754, 4.481646853389230856 ) ) ;
#19545=ADVANCED_FACE ( 'NONE', ( #56058 ), #12450, .T. ) ;
#19551=VERTEX_POINT ( 'NONE', #7201 ) ;
#19573=AXIS2_PLACEMENT_3D ( 'NONE', #14161, #60931, #62336 ) ;
#19583=CARTESIAN_POINT ( 'NONE',  ( -83.49999999999998579, -2.499999999999999556, 24.00000000000000000 ) ) ;
#19590=ORIENTED_EDGE ( 'NONE', *, *, #43009, .F. ) ;
#19592=DIRECTION ( 'NONE',  ( 1.000000000000000000, -1.189524669241239115E-16, 0.000000000000000000 ) ) ;
#19628=LINE ( 'NONE', #9440, #29731 ) ;
#19670=ORIENTED_EDGE ( 'NONE', *, *, #36755, .F. ) ;
#19694=DIRECTION ( 'NONE',  ( 0.000000000000000000, 0.000000000000000000, -1.000000000000000000 ) ) ;
#19729=ORIENTED_EDGE ( 'NONE', *, *, #25487, .T. ) ;
#19782=VERTEX_POINT ( 'NONE', #7021 ) ;
#19863=ORIENTED_EDGE ( 'NONE', *, *, #36940, .T. ) ;
#19875=ORIENTED_EDGE ( 'NONE', *, *, #49254, .F. ) ;
#19910=DIRECTION ( 'NONE',  ( -1.189524669241239115E-16, -1.000000000000000000, -0.000000000000000000 ) ) ;
#19937=ORIENTED_EDGE ( 'NONE', *, *, #44120, .F. ) ;
#19952=CARTESIAN_POINT ( 'NONE',  ( -12.16421356237309048, -4.000000000000000000, 18.58578643762690419 ) ) ;
#19960=CARTESIAN_POINT ( 'NONE',  ( -31.19338908182848513, -8.500000000001197265, 7.186868961050565829 ) ) ;
#19994=EDGE_CURVE ( 'NONE', #25847, #5343, #4137, .T. ) ;
#20044=ORIENTED_EDGE ( 'NONE', *, *, #34625, .T. ) ;
#20053=FACE_OUTER_BOUND ( 'NONE', #28230, .T. ) ;
#20054=CARTESIAN_POINT ( 'NONE',  ( -51.84221223720477667, -9.947368421052630083, 4.481646853389225527 ) ) ;
#20128=VERTEX_POINT ( 'NONE', #24830 ) ;
#20141=ORIENTED_EDGE ( 'NONE', *, *, #57202, .F. ) ;
#20168=LINE ( 'NONE', #63090, #43813 ) ;
#20242=ORIENTED_EDGE ( 'NONE', *, *, #21529, .F. ) ;
#20304=CARTESIAN_POINT ( 'NONE',  ( -33.89861118948982721, -9.947368421052624754, -2.000000000000000000 ) ) ;
#20317=CARTESIAN_POINT ( 'NONE',  ( -33.68474050223620964, -8.999709270181368126, 5.797011693762501139 ) ) ;
#20331=CARTESIAN_POINT ( 'NONE',  ( -75.75000000000000000, -0.9999999999999995559, 7.000000000000001776 ) ) ;
#20346=STYLED_ITEM ( 'NONE', ( #15983 ), #175 ) ;
#20352=CYLINDRICAL_SURFACE ( 'NONE', #51072, 3.100000000000003642 ) ;
#20367=VERTEX_POINT ( 'NONE', #9025 ) ;
#20372=AXIS2_PLACEMENT_3D ( 'NONE', #38235, #63872, #16764 ) ;
#20404=VERTEX_POINT ( 'NONE', #67766 ) ;
#20418=DIRECTION ( 'NONE',  ( 0.000000000000000000, 0.000000000000000000, 1.000000000000000000 ) ) ;
#20432=ADVANCED_FACE ( 'NONE', ( #17099 ), #32206, .F. ) ;
#20458=ORIENTED_EDGE ( 'NONE', *, *, #67682, .T. ) ;
#20467=CARTESIAN_POINT ( 'NONE',  ( -58.57530068368657794, -7.668632606274902841, -0.3315242760381541531 ) ) ;
#20538=PLANE ( 'NONE',  #36042 ) ;
#20539=DIRECTION ( 'NONE',  ( 1.000000000000000000, 0.000000000000000000, 0.000000000000000000 ) ) ;
#20571=AXIS2_PLACEMENT_3D ( 'NONE', #30939, #10194, #27020 ) ;
#20586=EDGE_CURVE ( 'NONE', #51601, #20128, #8935, .T. ) ;
#20590=VERTEX_POINT ( 'NONE', #61676 ) ;
#20624=UNCERTAINTY_MEASURE_WITH_UNIT (LENGTH_MEASURE( 1.000000000000000082E-05 ), #24748, 'distance_accuracy_value', 'NONE');
#20652=EDGE_CURVE ( 'NONE', #53553, #69054, #20168, .T. ) ;
#20670=ORIENTED_EDGE ( 'NONE', *, *, #53546, .F. ) ;
#20688=CARTESIAN_POINT ( 'NONE',  ( -41.74416970038988950, -12.08331763868298658, 3.200680680164544878 ) ) ;
#20689=VERTEX_POINT ( 'NONE', #34507 ) ;
#20715=FACE_OUTER_BOUND ( 'NONE', #53062, .T. ) ;
#20730=FACE_OUTER_BOUND ( 'NONE', #66054, .T. ) ;
#20740=VERTEX_POINT ( 'NONE', #28867 ) ;
#20742=EDGE_LOOP ( 'NONE', ( #34763, #20458, #53178, #34084, #60857, #56738, #4930 ) ) ;
#20773=CARTESIAN_POINT ( 'NONE',  ( -4.000000000000000000, -2.499999999999999556, 0.000000000000000000 ) ) ;
#20789=DIRECTION ( 'NONE',  ( -0.000000000000000000, -0.000000000000000000, -1.000000000000000000 ) ) ;
#20857=DIRECTION ( 'NONE',  ( 0.000000000000000000, 0.000000000000000000, 1.000000000000000000 ) ) ;
#20867=EDGE_LOOP ( 'NONE', ( #56275, #68341, #25591 ) ) ;
#20881=AXIS2_PLACEMENT_3D ( 'NONE', #23501, #930, #11925 ) ;
#20882=VECTOR ( 'NONE', #12350, 1000.000000000000000 ) ;
#20889=SURFACE_SIDE_STYLE ('',( #25801 ) ) ;
#20893=DIRECTION ( 'NONE',  ( -0.000000000000000000, 1.000000000000000000, -0.000000000000000000 ) ) ;
#21005=DIRECTION ( 'NONE',  ( 0.000000000000000000, 1.000000000000000000, 0.000000000000000000 ) ) ;
#21027=CARTESIAN_POINT ( 'NONE',  ( -11.74999999999999645, -0.9999999999999995559, 19.00000000000000000 ) ) ;
#21053=DIRECTION ( 'NONE',  ( 1.000000000000000000, 0.000000000000000000, 0.000000000000000000 ) ) ;
#21082=ORIENTED_EDGE ( 'NONE', *, *, #20586, .F. ) ;
#21117=CARTESIAN_POINT ( 'NONE',  ( -29.23998778563472811, -8.499999999999996447, 0.5867931367521921349 ) ) ;
#21141=VERTEX_POINT ( 'NONE', #56807 ) ;
#21149=CARTESIAN_POINT ( 'NONE',  ( -58.24585058642980329, -8.499999999999992895, 0.6021708693608249785 ) ) ;
#21218=ORIENTED_EDGE ( 'NONE', *, *, #17548, .T. ) ;
#21223=CIRCLE ( 'NONE', #35859, 2.500000000000000000 ) ;
#21226=ORIENTED_EDGE ( 'NONE', *, *, #14084, .T. ) ;
#21229=DIRECTION ( 'NONE',  ( 1.084202172485504434E-16, 1.000000000000000000, 0.000000000000000000 ) ) ;
#21241=CARTESIAN_POINT ( 'NONE',  ( -75.75000000000000000, -0.9999999999999995559, 19.00000000000000000 ) ) ;
#21262=TOROIDAL_SURFACE ( 'NONE', #61720, 2.000000000000000000, 1.000000000000000000 ) ;
#21308=FACE_OUTER_BOUND ( 'NONE', #33226, .T. ) ;
#21311=ORIENTED_EDGE ( 'NONE', *, *, #24463, .F. ) ;
#21323=VERTEX_POINT ( 'NONE', #39180 ) ;
#21342=EDGE_CURVE ( 'NONE', #48229, #6919, #56204, .T. ) ;
#21348=CARTESIAN_POINT ( 'NONE',  ( -31.03083116351206527, -8.500000000000001776, 7.024140319044499314 ) ) ;
#21372=CARTESIAN_POINT ( 'NONE',  ( -37.16661851630311730, -10.79484869592797658, 3.787717863381548256 ) ) ;
#21410=ORIENTED_EDGE ( 'NONE', *, *, #65268, .T. ) ;
#21418=AXIS2_PLACEMENT_3D ( 'NONE', #55317, #66577, #50071 ) ;
#21453=AXIS2_PLACEMENT_3D ( 'NONE', #58596, #31853, #16066 ) ;
#21489=LINE ( 'NONE', #43001, #63271 ) ;
#21507=CARTESIAN_POINT ( 'NONE',  ( -57.06152211476823766, -8.467913063795126760, -0.8045913523036769543 ) ) ;
#21529=EDGE_CURVE ( 'NONE', #32974, #19259, #26748, .T. ) ;
#21543=ORIENTED_EDGE ( 'NONE', *, *, #57101, .T. ) ;
#21574=CARTESIAN_POINT ( 'NONE',  ( -46.46651340543134978, -13.74896002192117095, 0.8313647636153821407 ) ) ;
#21583=PRESENTATION_STYLE_ASSIGNMENT (( #14950 ) ) ;
#21591=CARTESIAN_POINT ( 'NONE',  ( -43.75000000000000000, 0.000000000000000000, -5.100000000000000533 ) ) ;
#21597=LINE ( 'NONE', #43110, #55148 ) ;
#21603=LINE ( 'NONE', #1475, #26576 ) ;
#21607=DIRECTION ( 'NONE',  ( -0.000000000000000000, 1.000000000000000000, 0.000000000000000000 ) ) ;
#21621=DIRECTION ( 'NONE',  ( 0.000000000000000000, 0.000000000000000000, -1.000000000000000000 ) ) ;
#21630=AXIS2_PLACEMENT_3D ( 'NONE', #47983, #12446, #48660 ) ;
#21666=CIRCLE ( 'NONE', #20571, 1.000000000000000888 ) ;
#21667=CYLINDRICAL_SURFACE ( 'NONE', #30721, 1.000000000000000888 ) ;
#21779=LINE ( 'NONE', #42576, #563 ) ;
#21799=DIRECTION ( 'NONE',  ( 0.000000000000000000, 0.000000000000000000, 1.000000000000000000 ) ) ;
#21874=CARTESIAN_POINT ( 'NONE',  ( -54.73148258177010916, -9.107254030102707176, -2.000000000008438139 ) ) ;
#21892=CARTESIAN_POINT ( 'NONE',  ( -32.97523664431077606, -9.117691409006596359, -3.352975844304635356 ) ) ;
#21906=CARTESIAN_POINT ( 'NONE',  ( -87.50000000000000000, -8.499999999999989342, 1.000000000000000888 ) ) ;
#21925=CARTESIAN_POINT ( 'NONE',  ( -8.921435019309294474E-16, -7.500000000000000888, 0.000000000000000000 ) ) ;
#21934=CARTESIAN_POINT ( 'NONE',  ( -40.70406133565713702, -11.89285714285713880, 3.265330863013266693 ) ) ;
#21953=DIRECTION ( 'NONE',  ( 0.000000000000000000, 0.000000000000000000, -1.000000000000000000 ) ) ;
#21967=CARTESIAN_POINT ( 'NONE',  ( -57.11974195712093660, -8.499999999999992895, 8.000000000000000000 ) ) ;
#22018=CARTESIAN_POINT ( 'NONE',  ( -56.67268476622996332, -8.515503721524707359, -0.2436096942820924205 ) ) ;
#22027=FACE_OUTER_BOUND ( 'NONE', #4450, .T. ) ;
#22047=CARTESIAN_POINT ( 'NONE',  ( -71.75000000000000000, -4.000000000000000000, 20.00000000000000000 ) ) ;
#22060=CARTESIAN_POINT ( 'NONE',  ( -71.75000000000000000, -0.9999999999999995559, 20.00000000000000000 ) ) ;
#22070=CARTESIAN_POINT ( 'NONE',  ( -15.75000000000000000, -4.000000000000000000, 18.00000000000000000 ) ) ;
#22141=FACE_OUTER_BOUND ( 'NONE', #12819, .T. ) ;
#22142=FACE_OUTER_BOUND ( 'NONE', #53851, .T. ) ;
#22166=SHAPE_REPRESENTATION ( '8. Upper Jaw Support', ( #42840 ), #64177 ) ;
#22224=CARTESIAN_POINT ( 'NONE',  ( -43.75000000000000000, 0.000000000000000000, -3.500000000000002220 ) ) ;
#22241=EDGE_CURVE ( 'NONE', #20689, #52764, #25903, .T. ) ;
#22244=DIRECTION ( 'NONE',  ( -0.000000000000000000, -0.000000000000000000, 1.000000000000000000 ) ) ;
#22268=PLANE ( 'NONE',  #53032 ) ;
#22278=VERTEX_POINT ( 'NONE', #69513 ) ;
#22286=MECHANICAL_DESIGN_GEOMETRIC_PRESENTATION_REPRESENTATION('',(#859),#11080);
#22294=CARTESIAN_POINT ( 'NONE',  ( -34.31243252642735087, -10.02680648607962510, -3.499999999999997335 ) ) ;
#22305=DIRECTION ( 'NONE',  ( -1.000000000000000000, 0.000000000000000000, 0.000000000000000000 ) ) ;
#22350=CIRCLE ( 'NONE', #2031, 1.000000000000000888 ) ;
#22372=ORIENTED_EDGE ( 'NONE', *, *, #24509, .T. ) ;
#22445=CARTESIAN_POINT ( 'NONE',  ( -12.74999999999999822, -4.000000000000000000, 0.000000000000000000 ) ) ;
#22460=VERTEX_POINT ( 'NONE', #29365 ) ;
#22476=EDGE_LOOP ( 'NONE', ( #25494, #24050, #20670, #64791 ) ) ;
#22499=EDGE_LOOP ( 'NONE', ( #28871, #7338, #49190, #14934 ) ) ;
#22550=LINE ( 'NONE', #39113, #7717 ) ;
#22579=VERTEX_POINT ( 'NONE', #59134 ) ;
#22610=DIRECTION ( 'NONE',  ( -1.000000000000000000, 1.189524669241239115E-16, 0.000000000000000000 ) ) ;
#22616=FACE_OUTER_BOUND ( 'NONE', #67209, .T. ) ;
#22640=CARTESIAN_POINT ( 'NONE',  ( -34.75000000000000711, 0.000000000000000000, -7.000000000000000000 ) ) ;
#22680=CARTESIAN_POINT ( 'NONE',  ( -54.89978656749008223, -9.015750088250108263, -2.278575939223535851 ) ) ;
#22688=CYLINDRICAL_SURFACE ( 'NONE', #57815, 1.000000000000000000 ) ;
#22813=EDGE_CURVE ( 'NONE', #19551, #5309, #21666, .T. ) ;
#22841=EDGE_LOOP ( 'NONE', ( #30952, #16735, #57309, #50520 ) ) ;
#22865=DIRECTION ( 'NONE',  ( 0.000000000000000000, 0.000000000000000000, 1.000000000000000000 ) ) ;
#22898=ORIENTED_EDGE ( 'NONE', *, *, #51804, .T. ) ;
#22915=CARTESIAN_POINT ( 'NONE',  ( -54.89978656747977936, -9.015750088255273909, -2.278575939230922831 ) ) ;
#22946=ORIENTED_EDGE ( 'NONE', *, *, #37138, .T. ) ;
#22947=DIRECTION ( 'NONE',  ( 0.000000000000000000, 0.000000000000000000, 1.000000000000000000 ) ) ;
#22967=VECTOR ( 'NONE', #22244, 1000.000000000000000 ) ;
#22973=DIRECTION ( 'NONE',  ( 0.000000000000000000, 1.000000000000000000, 0.000000000000000000 ) ) ;
#22983=CARTESIAN_POINT ( 'NONE',  ( 3.081487911019577365E-31, -7.500000000000000888, 24.00000000000000000 ) ) ;
#22985=ORIENTED_EDGE ( 'NONE', *, *, #6344, .T. ) ;
#22992=CARTESIAN_POINT ( 'NONE',  ( -11.74999999999999645, -0.9999999999999995559, 7.000000000000001776 ) ) ;
#23032=CARTESIAN_POINT ( 'NONE',  ( -53.18756747357344494, -10.02680648607920588, -3.499999999999314326 ) ) ;
#23136=CARTESIAN_POINT ( 'NONE',  ( -36.34584199317021103, -11.88577921580104579, 1.495499336507959853 ) ) ;
#23192=VERTEX_POINT ( 'NONE', #24874 ) ;
#23195=CARTESIAN_POINT ( 'NONE',  ( -41.30760631258792870, -13.80057017807656550, 0.8185668606472049635 ) ) ;
#23284=VERTEX_POINT ( 'NONE', #25564 ) ;
#23307=CARTESIAN_POINT ( 'NONE',  ( -9.908575283019910450E-16, -6.500000000000000888, 0.000000000000000000 ) ) ;
#23363=DIRECTION ( 'NONE',  ( -0.000000000000000000, -0.000000000000000000, 1.000000000000000000 ) ) ;
#23393=CARTESIAN_POINT ( 'NONE',  ( -57.09597854763558900, -7.829934782661390535, -1.044957726401560594 ) ) ;
#23428=EDGE_CURVE ( 'NONE', #46008, #42263, #840, .T. ) ;
#23498=CARTESIAN_POINT ( 'NONE',  ( -69.74999999999998579, -4.000000000000000000, 20.00000000000000000 ) ) ;
#23501=CARTESIAN_POINT ( 'NONE',  ( -12.74999999999999822, -0.9999999999999995559, 5.000000000000001776 ) ) ;
#23506=DIRECTION ( 'NONE',  ( -7.703719777548941223E-32, 1.000000000000000000, 0.000000000000000000 ) ) ;
#23528=AXIS2_PLACEMENT_3D ( 'NONE', #12122, #42818, #27593 ) ;
#23538=CARTESIAN_POINT ( 'NONE',  ( -28.03849660526295295, -8.499999999999996447, 0.9189689158111923328 ) ) ;
#23565=CARTESIAN_POINT ( 'NONE',  ( -12.74999999999999822, -3.000000000000000000, 7.000000000000001776 ) ) ;
#23571=EDGE_LOOP ( 'NONE', ( #13051, #9931, #20141, #18317 ) ) ;
#23592=ORIENTED_EDGE ( 'NONE', *, *, #44539, .T. ) ;
#23632=LINE ( 'NONE', #28894, #46056 ) ;
#23645=VERTEX_POINT ( 'NONE', #68090 ) ;
#23646=AXIS2_PLACEMENT_3D ( 'NONE', #51690, #2758, #24247 ) ;
#23677=DIRECTION ( 'NONE',  ( 0.000000000000000000, 0.000000000000000000, -1.000000000000000000 ) ) ;
#23685=VECTOR ( 'NONE', #50575, 1000.000000000000000 ) ;
#23693=CARTESIAN_POINT ( 'NONE',  ( -49.29458994068759381, -11.22445319598486435, 3.543713891411715000 ) ) ;
#23706=DIRECTION ( 'NONE',  ( 0.000000000000000000, 0.000000000000000000, 1.000000000000000000 ) ) ;
#23715=FACE_OUTER_BOUND ( 'NONE', #57047, .T. ) ;
#23736=CARTESIAN_POINT ( 'NONE',  ( -50.46281877639898283, -12.29960362420287012, 1.307293633603369809 ) ) ;
#23745=ADVANCED_FACE ( 'NONE', ( #65557 ), #65454, .T. ) ;
#23751=CARTESIAN_POINT ( 'NONE',  ( -43.75000000000000000, 0.000000000000000000, 0.000000000000000000 ) ) ;
#23789=ORIENTED_EDGE ( 'NONE', *, *, #9558, .F. ) ;
#23795=ORIENTED_EDGE ( 'NONE', *, *, #8917, .F. ) ;
#23826=CARTESIAN_POINT ( 'NONE',  ( -12.74999999999999822, -4.000000000000000000, 18.00000000000000000 ) ) ;
#23853=DIRECTION ( 'NONE',  ( 0.000000000000000000, 0.000000000000000000, 1.000000000000000000 ) ) ;
#23877=ORIENTED_EDGE ( 'NONE', *, *, #57660, .F. ) ;
#23892=CARTESIAN_POINT ( 'NONE',  ( -29.43102036153494439, -7.714630622815294103, -0.5236166406898870029 ) ) ;
#23914=ORIENTED_EDGE ( 'NONE', *, *, #9466, .T. ) ;
#23925=EDGE_LOOP ( 'NONE', ( #913, #19670, #48056, #58578 ) ) ;
#23968=AXIS2_PLACEMENT_3D ( 'NONE', #12886, #66710, #29037 ) ;
#23998=EDGE_LOOP ( 'NONE', ( #17415, #8569, #30133, #27386 ) ) ;
#23999=LINE ( 'NONE', #39878, #67637 ) ;
#24036=CARTESIAN_POINT ( 'NONE',  ( -71.75000000000000000, 4.336808689942018722E-16, 19.00000000000000000 ) ) ;
#24044=FACE_OUTER_BOUND ( 'NONE', #35562, .T. ) ;
#24050=ORIENTED_EDGE ( 'NONE', *, *, #11129, .T. ) ;
#24067=EDGE_CURVE ( 'NONE', #42007, #25839, #45056, .T. ) ;
#24098=CARTESIAN_POINT ( 'NONE',  ( -55.75572903516371071, -8.276929449822308271, -1.923638504044224318 ) ) ;
#24109=LINE ( 'NONE', #45613, #37733 ) ;
#24184=CARTESIAN_POINT ( 'NONE',  ( -16.75000000000000000, -4.000000000000000000, 20.00000000000000000 ) ) ;
#24196=CYLINDRICAL_SURFACE ( 'NONE', #61450, 3.100000000000003642 ) ;
#24199=VERTEX_POINT ( 'NONE', #53294 ) ;
#24223=EDGE_CURVE ( 'NONE', #6919, #51912, #38485, .T. ) ;
#24238=CARTESIAN_POINT ( 'NONE',  ( -30.01048380477565658, -8.499999999999998224, -0.6003161102123087955 ) ) ;
#24245=DIRECTION ( 'NONE',  ( 0.000000000000000000, 0.000000000000000000, 1.000000000000000000 ) ) ;
#24247=DIRECTION ( 'NONE',  ( -1.000000000000000000, 0.000000000000000000, -0.000000000000000000 ) ) ;
#24257=CIRCLE ( 'NONE', #57972, 0.9999999999999995559 ) ;
#24279=TOROIDAL_SURFACE ( 'NONE', #2754, 18.53939201416945082, 5.000000000000000000 ) ;
#24298=ORIENTED_EDGE ( 'NONE', *, *, #332, .T. ) ;
#24322=LINE ( 'NONE', #28890, #43732 ) ;
#24336=CARTESIAN_POINT ( 'NONE',  ( -11.99999999999999822, -6.499999999999999112, 3.000000000000000000 ) ) ;
#24378=DIRECTION ( 'NONE',  ( 0.000000000000000000, 0.000000000000000000, -1.000000000000000000 ) ) ;
#24404=ORIENTED_EDGE ( 'NONE', *, *, #47948, .F. ) ;
#24429=AXIS2_PLACEMENT_3D ( 'NONE', #31679, #26049, #53157 ) ;
#24463=EDGE_CURVE ( 'NONE', #1828, #1406, #2529, .T. ) ;
#24488=CARTESIAN_POINT ( 'NONE',  ( 0.000000000000000000, 0.000000000000000000, 0.000000000000000000 ) ) ;
#24509=EDGE_CURVE ( 'NONE', #26721, #29573, #63186, .T. ) ;
#24513=ORIENTED_EDGE ( 'NONE', *, *, #14530, .T. ) ;
#24524=CARTESIAN_POINT ( 'NONE',  ( -53.42555371347750537, -9.981032396169707610, -3.023059613375645327 ) ) ;
#24534=FACE_OUTER_BOUND ( 'NONE', #58222, .T. ) ;
#24552=CARTESIAN_POINT ( 'NONE',  ( -87.50000000000000000, -7.499999999999990230, 1.000000000000000000 ) ) ;
#24557=EDGE_CURVE ( 'NONE', #19551, #49493, #46591, .T. ) ;
#24594=VERTEX_POINT ( 'NONE', #52875 ) ;
#24618=ORIENTED_EDGE ( 'NONE', *, *, #27307, .T. ) ;
#24633=CARTESIAN_POINT ( 'NONE',  ( -71.75000000000000000, 4.336808689942018722E-16, 24.00000000000000000 ) ) ;
#24642=AXIS2_PLACEMENT_3D ( 'NONE', #27837, #44456, #6407 ) ;
#24645=VECTOR ( 'NONE', #15979, 1000.000000000000000 ) ;
#24676=CARTESIAN_POINT ( 'NONE',  ( -57.48951619522305378, -8.499999999999996447, -0.6003161102129058735 ) ) ;
#24677=ORIENTED_EDGE ( 'NONE', *, *, #38883, .F. ) ;
#24679=EDGE_CURVE ( 'NONE', #51004, #49493, #19328, .T. ) ;
#24685=CARTESIAN_POINT ( 'NONE',  ( -43.75000000000000000, -13.49999999999999645, 8.000000000000000000 ) ) ;
#24704=ORIENTED_EDGE ( 'NONE', *, *, #3914, .F. ) ;
#24717=ORIENTED_EDGE ( 'NONE', *, *, #44604, .T. ) ;
#24748=( LENGTH_UNIT ( ) NAMED_UNIT ( * ) SI_UNIT ( .MILLI., .METRE. ) );
#24762=( LENGTH_UNIT ( ) NAMED_UNIT ( * ) SI_UNIT ( .MILLI., .METRE. ) );
#24799=CARTESIAN_POINT ( 'NONE',  ( -1.011095968855053334E-15, -8.500000000000000000, 21.00000000000000000 ) ) ;
#24830=CARTESIAN_POINT ( 'NONE',  ( -70.75000000000000000, -3.000000000000000000, 20.00000000000000000 ) ) ;
#24874=CARTESIAN_POINT ( 'NONE',  ( -11.74999999999999645, -3.000000000000000000, 19.00000000000000000 ) ) ;
#24887=VECTOR ( 'NONE', #61832, 1000.000000000000000 ) ;
#24916=VERTEX_POINT ( 'NONE', #8822 ) ;
#24934=LINE ( 'NONE', #10159, #8388 ) ;
#24944=AXIS2_PLACEMENT_3D ( 'NONE', #29968, #51431, #14151 ) ;
#24960=EDGE_LOOP ( 'NONE', ( #61281, #25553, #4358, #36786 ) ) ;
#24983=VECTOR ( 'NONE', #5841, 1000.000000000000000 ) ;
#24999=CARTESIAN_POINT ( 'NONE',  ( -55.47676709573605081, -8.704246530741306387, 6.357025138608363157 ) ) ;
#25082=ORIENTED_EDGE ( 'NONE', *, *, #11006, .F. ) ;
#25112=AXIS2_PLACEMENT_3D ( 'NONE', #59691, #16136, #37260 ) ;
#25123=CARTESIAN_POINT ( 'NONE',  ( -26.79538245034556354, -7.499999999999999112, 0.000000000000000000 ) ) ;
#25129=CARTESIAN_POINT ( 'NONE',  ( -58.75000000000000000, -4.000000000000000000, 11.89999999999999680 ) ) ;
#25135=AXIS2_PLACEMENT_3D ( 'NONE', #323, #47606, #41965 ) ;
#25150=CARTESIAN_POINT ( 'NONE',  ( -37.17007440505049942, -12.37226643102196633, 1.277129481866865035 ) ) ;
#25170=ORIENTED_EDGE ( 'NONE', *, *, #54583, .F. ) ;
#25174=CIRCLE ( 'NONE', #65638, 18.53939201416945082 ) ;
#25197=EDGE_CURVE ( 'NONE', #40324, #61550, #34425, .T. ) ;
#25209=CARTESIAN_POINT ( 'NONE',  ( -32.62570226935650197, -8.499999999999996447, 8.000000000000000000 ) ) ;
#25219=LINE ( 'NONE', #31167, #65265 ) ;
#25227=ORIENTED_EDGE ( 'NONE', *, *, #57101, .F. ) ;
#25235=( BOUNDED_SURFACE ( )  B_SPLINE_SURFACE ( 3, 2, ( 
 ( #21934, #65524, #37813 ),
 ( #53588, #12384, #64496 ),
 ( #39171, #32825, #6424 ),
 ( #54265, #48702, #43445 ),
 ( #54942, #44121, #5372 ),
 ( #6087, #17373, #27519 ),
 ( #49045, #736, #60249 ),
 ( #12045, #65167, #21574 ),
 ( #17012, #16340, #40 ),
 ( #59895, #11713, #59185 ) ),
 .UNSPECIFIED., .F., .F., .F. ) 
 B_SPLINE_SURFACE_WITH_KNOTS ( ( 4, 2, 2, 2, 4 ),
 ( 3, 3 ),
 ( 0.01935955400260480630, 0.02095281869284682311, 0.02254608338308883991, 0.02413934807333086019, 0.02573261276357287700 ),
 ( 0.000000000000000000, 1.000000000000000000 ),
 .UNSPECIFIED. ) 
 GEOMETRIC_REPRESENTATION_ITEM ( )  RATIONAL_B_SPLINE_SURFACE ( (
 ( 1.000000000000000000, 0.8093049424017613180, 1.000000000000000000),
 ( 1.000000000000000000, 0.8049424280649992713, 1.000000000000000000),
 ( 1.000000000000000000, 0.8014042547541196937, 1.000000000000000000),
 ( 1.000000000000000000, 0.7967637600457907476, 1.000000000000000000),
 ( 1.000000000000000000, 0.7956476677631215688, 1.000000000000000000),
 ( 1.000000000000000000, 0.7960422929644409562, 1.000000000000000000),
 ( 1.000000000000000000, 0.7975419603936064750, 1.000000000000000000),
 ( 1.000000000000000000, 0.8027988638271628119, 1.000000000000000000),
 ( 1.000000000000000000, 0.8065519299663326258, 1.000000000000000000),
 ( 1.000000000000000000, 0.8111477107414843957, 1.000000000000000000) ) ) 
 REPRESENTATION_ITEM ( '' )  SURFACE ( )  );
#25253=DIRECTION ( 'NONE',  ( -1.000000000000000000, 1.189524669241239115E-16, 0.000000000000000000 ) ) ;
#25266=ORIENTED_EDGE ( 'NONE', *, *, #64319, .F. ) ;
#25287=DIRECTION ( 'NONE',  ( 0.000000000000000000, 0.000000000000000000, 1.000000000000000000 ) ) ;
#25288=CARTESIAN_POINT ( 'NONE',  ( -70.75000000000000000, -4.000000000000000000, 19.00000000000000000 ) ) ;
#25294=VECTOR ( 'NONE', #46273, 1000.000000000000000 ) ;
#25309=CARTESIAN_POINT ( 'NONE',  ( -76.75000000000000000, 4.336808689942018722E-16, 7.000000000000001776 ) ) ;
#25318=AXIS2_PLACEMENT_3D ( 'NONE', #37606, #5179, #6550 ) ;
#25319=LINE ( 'NONE', #52083, #9657 ) ;
#25323=EDGE_CURVE ( 'NONE', #25898, #33970, #36559, .T. ) ;
#25349=CARTESIAN_POINT ( 'NONE',  ( -53.83246130318194389, -9.718525487688895126, 3.069079019093576388 ) ) ;
#25360=VERTEX_POINT ( 'NONE', #1134 ) ;
#25362=CARTESIAN_POINT ( 'NONE',  ( -33.14152459314272647, -9.158144248744079619, -2.873992752689456864 ) ) ;
#25366=VECTOR ( 'NONE', #37024, 1000.000000000000000 ) ;
#25377=CARTESIAN_POINT ( 'NONE',  ( -33.77766424705443882, -9.706441239724112435, -3.029717036663232221 ) ) ;
#25402=AXIS2_PLACEMENT_3D ( 'NONE', #23565, #34812, #45076 ) ;
#25409=PRODUCT_DEFINITION_SHAPE ( 'NONE', 'NONE',  #67906 ) ;
#25416=CARTESIAN_POINT ( 'NONE',  ( -58.75000000000000000, -8.499999999999992895, 18.10000000000000497 ) ) ;
#25432=CARTESIAN_POINT ( 'NONE',  ( -12.74999999999999822, 0.000000000000000000, 6.000000000000001776 ) ) ;
#25472=DIRECTION ( 'NONE',  ( -0.000000000000000000, 0.000000000000000000, 1.000000000000000000 ) ) ;
#25487=EDGE_CURVE ( 'NONE', #3527, #32747, #27902, .T. ) ;
#25494=ORIENTED_EDGE ( 'NONE', *, *, #61347, .F. ) ;
#25519=FACE_OUTER_BOUND ( 'NONE', #55106, .T. ) ;
#25543=CARTESIAN_POINT ( 'NONE',  ( -27.87363414264613937, -7.580382958994807296, -0.06854651313594288531 ) ) ;
#25547=ORIENTED_EDGE ( 'NONE', *, *, #30734, .F. ) ;
#25553=ORIENTED_EDGE ( 'NONE', *, *, #31362, .T. ) ;
#25564=CARTESIAN_POINT ( 'NONE',  ( -30.38025804287905629, -8.499999999999996447, 0.06931351858032895608 ) ) ;
#25591=ORIENTED_EDGE ( 'NONE', *, *, #24679, .F. ) ;
#25629=CARTESIAN_POINT ( 'NONE',  ( -84.49999999999998579, -3.499999999999999556, 0.000000000000000000 ) ) ;
#25633=CARTESIAN_POINT ( 'NONE',  ( -1.011095968855053334E-15, -8.500000000000000000, 21.00000000000000000 ) ) ;
#25635=( BOUNDED_SURFACE ( )  B_SPLINE_SURFACE ( 3, 2, ( 
 ( #611, #43628, #65024 ),
 ( #33041, #8722, #13641 ),
 ( #3389, #35104, #46040 ),
 ( #24524, #62520, #66779 ),
 ( #30151, #51289, #40402 ),
 ( #67818, #51632, #18594 ) ),
 .UNSPECIFIED., .F., .F., .F. ) 
 B_SPLINE_SURFACE_WITH_KNOTS ( ( 4, 2, 4 ),
 ( 3, 3 ),
 ( 0.03640205491000769733, 0.03794596731985258597, 0.03948987972969747462 ),
 ( 0.000000000000000000, 0.3658361493744603510 ),
 .UNSPECIFIED. ) 
 GEOMETRIC_REPRESENTATION_ITEM ( )  RATIONAL_B_SPLINE_SURFACE ( (
 ( 1.000000000000000000, 0.9724907272181566587, 0.9651092272895156476),
 ( 1.000000000000000000, 0.9724900729383123554, 0.9651083974482648209),
 ( 1.000000000000000000, 0.9723552707549931728, 0.9649374241049719636),
 ( 1.000000000000000000, 0.9718243316192900494, 0.9642640192914814223),
 ( 1.000000000000000000, 0.9714236478976183697, 0.9637558210278448501),
 ( 1.000000000000000000, 0.9708971511394390852, 0.9630880506048271616) ) ) 
 REPRESENTATION_ITEM ( '' )  SURFACE ( )  );
#25648=DIRECTION ( 'NONE',  ( 0.000000000000000000, 0.000000000000000000, -1.000000000000000000 ) ) ;
#25649=EDGE_LOOP ( 'NONE', ( #3036, #34387, #1562, #9806, #7331, #65232 ) ) ;
#25690=DIRECTION ( 'NONE',  ( -0.000000000000000000, -1.000000000000000000, -0.000000000000000000 ) ) ;
#25692=ORIENTED_EDGE ( 'NONE', *, *, #25869, .T. ) ;
#25738=CARTESIAN_POINT ( 'NONE',  ( -10.74999999999999645, 4.336808689942018722E-16, 19.00000000000000000 ) ) ;
#25746=EDGE_CURVE ( 'NONE', #5856, #59351, #59810, .T. ) ;
#25801=SURFACE_STYLE_FILL_AREA ( #27162 ) ;
#25808=ORIENTED_EDGE ( 'NONE', *, *, #47413, .T. ) ;
#25839=VERTEX_POINT ( 'NONE', #21906 ) ;
#25844=EDGE_LOOP ( 'NONE', ( #64522, #68249, #29526, #6520 ) ) ;
#25847=VERTEX_POINT ( 'NONE', #56684 ) ;
#25853=CARTESIAN_POINT ( 'NONE',  ( 0.000000000000000000, -3.000000000000000000, 18.00000000000000000 ) ) ;
#25869=EDGE_CURVE ( 'NONE', #51601, #4575, #5912, .T. ) ;
#25891=MECHANICAL_DESIGN_GEOMETRIC_PRESENTATION_REPRESENTATION('',(#12431),#29255);
#25894=CARTESIAN_POINT ( 'NONE',  ( -28.91790128120562997, -7.668906119302852709, -0.3459828814411498032 ) ) ;
#25898=VERTEX_POINT ( 'NONE', #28881 ) ;
#25903=LINE ( 'NONE', #48110, #15988 ) ;
#25905=ORIENTED_EDGE ( 'NONE', *, *, #30461, .F. ) ;
#25908=CARTESIAN_POINT ( 'NONE',  ( 1.189524669241243060E-16, -7.500000000000000888, 23.00000000000000000 ) ) ;
#25909=ORIENTED_EDGE ( 'NONE', *, *, #64239, .F. ) ;
#25949=AXIS2_PLACEMENT_3D ( 'NONE', #13650, #1986, #23506 ) ;
#26026=CYLINDRICAL_SURFACE ( 'NONE', #47788, 1.000000000000000888 ) ;
#26049=DIRECTION ( 'NONE',  ( -1.000000000000000000, -0.000000000000000000, -0.000000000000000000 ) ) ;
#26057=CARTESIAN_POINT ( 'NONE',  ( -58.75000000000000000, -8.499999999999992895, 15.00000000000000178 ) ) ;
#26078=CARTESIAN_POINT ( 'NONE',  ( -58.07111477172493608, -7.714422322210367611, -0.5225021303434840281 ) ) ;
#26118=ORIENTED_EDGE ( 'NONE', *, *, #57202, .T. ) ;
#26180=CARTESIAN_POINT ( 'NONE',  ( -75.75000000000000000, -0.4142135623730948124, 19.00000000000000000 ) ) ;
#26187=EDGE_CURVE ( 'NONE', #23284, #35896, #14542, .T. ) ;
#26208=CIRCLE ( 'NONE', #42041, 1.000000000000000000 ) ;
#26214=CARTESIAN_POINT ( 'NONE',  ( -11.74999999999999645, -4.000000000000000000, 7.000000000000001776 ) ) ;
#26255=CIRCLE ( 'NONE', #55435, 1.999999999999999112 ) ;
#26270=CYLINDRICAL_SURFACE ( 'NONE', #52413, 1.000000000000000888 ) ;
#26308=AXIS2_PLACEMENT_3D ( 'NONE', #15531, #25690, #37001 ) ;
#26340=AXIS2_PLACEMENT_3D ( 'NONE', #28483, #29896, #29544 ) ;
#26367=VERTEX_POINT ( 'NONE', #55184 ) ;
#26404=DIRECTION ( 'NONE',  ( 0.000000000000000000, 0.000000000000000000, 1.000000000000000000 ) ) ;
#26418=ORIENTED_EDGE ( 'NONE', *, *, #3718, .F. ) ;
#26451=EDGE_CURVE ( 'NONE', #25847, #25839, #26208, .T. ) ;
#26478=CYLINDRICAL_SURFACE ( 'NONE', #30234, 1.000000000000000888 ) ;
#26487=VECTOR ( 'NONE', #46135, 1000.000000000000000 ) ;
#26495=FACE_OUTER_BOUND ( 'NONE', #20742, .T. ) ;
#26508=EDGE_CURVE ( 'NONE', #46008, #43417, #3727, .T. ) ;
#26541=DIRECTION ( 'NONE',  ( 0.000000000000000000, 0.000000000000000000, -1.000000000000000000 ) ) ;
#26559=CARTESIAN_POINT ( 'NONE',  ( -83.49999999999998579, 4.336808689942018722E-16, -0.000000000000000000 ) ) ;
#26576=VECTOR ( 'NONE', #37499, 1000.000000000000000 ) ;
#26578=EDGE_CURVE ( 'NONE', #20367, #23192, #37956, .T. ) ;
#26581=ORIENTED_EDGE ( 'NONE', *, *, #702, .T. ) ;
#26595=ORIENTED_EDGE ( 'NONE', *, *, #57470, .F. ) ;
#26615=LINE ( 'NONE', #10812, #31907 ) ;
#26616=CARTESIAN_POINT ( 'NONE',  ( -31.68092575729820126, -8.628515624790352945, 6.048998428370452984 ) ) ;
#26634=VERTEX_POINT ( 'NONE', #58320 ) ;
#26637=CARTESIAN_POINT ( 'NONE',  ( -37.58704975911827262, -10.98121406184487192, 3.676737808024616694 ) ) ;
#26648=FACE_OUTER_BOUND ( 'NONE', #11166, .T. ) ;
#26696=ORIENTED_EDGE ( 'NONE', *, *, #44376, .F. ) ;
#26717=CARTESIAN_POINT ( 'NONE',  ( -28.03849660521344234, -8.499999999999996447, 0.9189689155263818243 ) ) ;
#26721=VERTEX_POINT ( 'NONE', #7613 ) ;
#26748=LINE ( 'NONE', #9925, #65256 ) ;
#26768=ORIENTED_EDGE ( 'NONE', *, *, #14530, .F. ) ;
#26777=CARTESIAN_POINT ( 'NONE',  ( -33.70169882663748950, -9.480064694312421381, -3.454096298675830123 ) ) ;
#26806=ORIENTED_EDGE ( 'NONE', *, *, #52842, .F. ) ;
#26819=EDGE_CURVE ( 'NONE', #32974, #11830, #46557, .T. ) ;
#26823=DIRECTION ( 'NONE',  ( 1.000000000000000000, -1.189524669241239115E-16, 0.000000000000000000 ) ) ;
#26826=CARTESIAN_POINT ( 'NONE',  ( -84.49999999999998579, -2.499999999999999556, 24.00000000000000000 ) ) ;
#26828=CARTESIAN_POINT ( 'NONE',  ( -74.75000000000000000, -0.9999999999999995559, 7.000000000000001776 ) ) ;
#26888=VECTOR ( 'NONE', #19910, 1000.000000000000000 ) ;
#26897=EDGE_CURVE ( 'NONE', #53553, #59113, #69483, .T. ) ;
#26910=VECTOR ( 'NONE', #59454, 1000.000000000000000 ) ;
#26935=ORIENTED_EDGE ( 'NONE', *, *, #53607, .T. ) ;
#26939=FACE_OUTER_BOUND ( 'NONE', #62920, .T. ) ;
#26956=CARTESIAN_POINT ( 'NONE',  ( -87.50000000000000000, -3.500000000000000000, 0.000000000000000000 ) ) ;
#26961=DIRECTION ( 'NONE',  ( 1.000000000000000000, 0.000000000000000000, 0.000000000000000000 ) ) ;
#27020=DIRECTION ( 'NONE',  ( 0.000000000000000000, 0.000000000000000000, -1.000000000000000000 ) ) ;
#27033=CARTESIAN_POINT ( 'NONE',  ( -43.75000000000000000, 0.000000000000000000, -2.000000000000000000 ) ) ;
#27039=DIRECTION ( 'NONE',  ( -1.000000000000000000, 0.000000000000000000, -0.000000000000000000 ) ) ;
#27056=ADVANCED_FACE ( 'NONE', ( #50127 ), #22688, .F. ) ;
#27067=LINE ( 'NONE', #15202, #54840 ) ;
#27068=DIRECTION ( 'NONE',  ( 0.000000000000000000, 0.000000000000000000, 1.000000000000000000 ) ) ;
#27069=DIRECTION ( 'NONE',  ( -0.000000000000000000, 1.000000000000000000, 0.000000000000000000 ) ) ;
#27080=VECTOR ( 'NONE', #13178, 1000.000000000000000 ) ;
#27146=FACE_OUTER_BOUND ( 'NONE', #4208, .T. ) ;
#27151=EDGE_LOOP ( 'NONE', ( #3962, #15145, #24513, #66202 ) ) ;
#27155=EDGE_CURVE ( 'NONE', #10026, #4254, #11781, .T. ) ;
#27162=FILL_AREA_STYLE ('',( #15300 ) ) ;
#27242=AXIS2_PLACEMENT_3D ( 'NONE', #49017, #12030, #27498 ) ;
#27249=B_SPLINE_CURVE_WITH_KNOTS ( 'NONE', 3,
 ( #22294, #37498, #48380, #16707, #5403, #38170 ),
 .UNSPECIFIED., .F., .F.,
 ( 4, 2, 4 ),
 ( 5.235446031985231014E-16, 0.0007919337925127429125, 0.001583867585024962155 ),
 .UNSPECIFIED. ) ;
#27253=CARTESIAN_POINT ( 'NONE',  ( -56.05026940434684946, -8.611541138641610971, -0.7530887220977782182 ) ) ;
#27259=ORIENTED_EDGE ( 'NONE', *, *, #24223, .T. ) ;
#27278=AXIS2_PLACEMENT_3D ( 'NONE', #17762, #50805, #45212 ) ;
#27298=ORIENTED_EDGE ( 'NONE', *, *, #31912, .T. ) ;
#27307=EDGE_CURVE ( 'NONE', #17714, #52764, #54421, .T. ) ;
#27327=CARTESIAN_POINT ( 'NONE',  ( -35.65778776279520912, -8.171052631578938019, 2.722470280083845395 ) ) ;
#27386=ORIENTED_EDGE ( 'NONE', *, *, #50176, .F. ) ;
#27388=EDGE_CURVE ( 'NONE', #66384, #13277, #66572, .T. ) ;
#27429=ADVANCED_FACE ( 'NONE', ( #61500 ), #19142, .T. ) ;
#27447=LINE ( 'NONE', #11982, #66781 ) ;
#27470=CARTESIAN_POINT ( 'NONE',  ( -57.11974195712093660, -8.499999999999992895, 8.000000000000000000 ) ) ;
#27477=VECTOR ( 'NONE', #68777, 1000.000000000000000 ) ;
#27498=DIRECTION ( 'NONE',  ( -0.2648642316819883047, 0.9642857142857141906, 0.000000000000000000 ) ) ;
#27519=CARTESIAN_POINT ( 'NONE',  ( -44.55113387769600308, -13.99226303593487408, 0.7733428766569989676 ) ) ;
#27521=CARTESIAN_POINT ( 'NONE',  ( -28.74999999999999645, -13.99999999999999822, 18.10000000000000497 ) ) ;
#27548=ORIENTED_EDGE ( 'NONE', *, *, #13568, .F. ) ;
#27567=ORIENTED_EDGE ( 'NONE', *, *, #13568, .T. ) ;
#27593=DIRECTION ( 'NONE',  ( 1.000000000000000000, 0.000000000000000000, 0.000000000000000000 ) ) ;
#27601=CARTESIAN_POINT ( 'NONE',  ( -29.98030399291527459, 0.000000000000000000, -3.499999999999998668 ) ) ;
#27626=ORIENTED_EDGE ( 'NONE', *, *, #22241, .F. ) ;
#27647=ORIENTED_EDGE ( 'NONE', *, *, #9965, .F. ) ;
#27749=DIRECTION ( 'NONE',  ( -0.000000000000000000, 1.000000000000000000, -0.000000000000000000 ) ) ;
#27769=ORIENTED_EDGE ( 'NONE', *, *, #32471, .T. ) ;
#27813=CARTESIAN_POINT ( 'NONE',  ( -32.76090269711983893, -9.103122581850293216, -2.000000000000000000 ) ) ;
#27830=LINE ( 'NONE', #59515, #22967 ) ;
#27834=PLANE ( 'NONE',  #46316 ) ;
#27837=CARTESIAN_POINT ( 'NONE',  ( -16.75000000000000000, -4.000000000000000000, 19.00000000000000000 ) ) ;
#27850=EDGE_CURVE ( 'NONE', #17478, #62302, #33842, .T. ) ;
#27863=CARTESIAN_POINT ( 'NONE',  ( -43.75000000000000000, 0.000000000000000000, -7.000000000000000000 ) ) ;
#27864=ORIENTED_EDGE ( 'NONE', *, *, #28000, .T. ) ;
#27902=LINE ( 'NONE', #52697, #56387 ) ;
#27912=ORIENTED_EDGE ( 'NONE', *, *, #49254, .T. ) ;
#27938=DIRECTION ( 'NONE',  ( 0.000000000000000000, 0.000000000000000000, 1.000000000000000000 ) ) ;
#27942=CARTESIAN_POINT ( 'NONE',  ( -52.82340657583479526, -10.67641508236616943, 2.169052831005622295 ) ) ;
#27948=EDGE_CURVE ( 'NONE', #5309, #29847, #62292, .T. ) ;
#27972=ORIENTED_EDGE ( 'NONE', *, *, #44376, .T. ) ;
#27983=ADVANCED_FACE ( 'NONE', ( #47562 ), #68272, .F. ) ;
#27993=ADVANCED_FACE ( 'NONE', ( #15186 ), #6594, .T. ) ;
#28000=EDGE_CURVE ( 'NONE', #22460, #51117, #6883, .T. ) ;
#28118=FACE_OUTER_BOUND ( 'NONE', #23998, .T. ) ;
#28146=DIRECTION ( 'NONE',  ( 0.000000000000000000, 0.000000000000000000, -1.000000000000000000 ) ) ;
#28151=CARTESIAN_POINT ( 'NONE',  ( -34.07444628652228857, -9.981032396169499776, -3.023059613375652876 ) ) ;
#28158=AXIS2_PLACEMENT_3D ( 'NONE', #25908, #47432, #5472 ) ;
#28194=DIRECTION ( 'NONE',  ( -1.000000000000000000, 0.000000000000000000, 0.000000000000000000 ) ) ;
#28208=DIRECTION ( 'NONE',  ( 1.000000000000000000, 0.000000000000000000, -0.000000000000000000 ) ) ;
#28209=CIRCLE ( 'NONE', #14821, 3.100000000000001865 ) ;
#28230=EDGE_LOOP ( 'NONE', ( #10373, #56114, #54203, #11515 ) ) ;
#28266=CARTESIAN_POINT ( 'NONE',  ( -16.75000000000000000, -4.000000000000000000, 24.00000000000000000 ) ) ;
#28284=DIRECTION ( 'NONE',  ( -1.000000000000000000, 0.000000000000000000, 0.000000000000000000 ) ) ;
#28298=CARTESIAN_POINT ( 'NONE',  ( -54.93556801395976663, -8.762778093175660032, -2.499999999999992895 ) ) ;
#28362=CARTESIAN_POINT ( 'NONE',  ( -39.71230376710084187, -11.68673171624858931, 3.338102362379923083 ) ) ;
#28394=EDGE_CURVE ( 'NONE', #54981, #18574, #29494, .T. ) ;
#28407=CYLINDRICAL_SURFACE ( 'NONE', #158, 1.000000000000000888 ) ;
#28409=ORIENTED_EDGE ( 'NONE', *, *, #15906, .T. ) ;
#28474=EDGE_CURVE ( 'NONE', #45120, #21141, #63917, .T. ) ;
#28483=CARTESIAN_POINT ( 'NONE',  ( -69.74999999999998579, -3.000000000000000000, 20.00000000000000000 ) ) ;
#28502=CIRCLE ( 'NONE', #47728, 1.999999999999998224 ) ;
#28530=EDGE_LOOP ( 'NONE', ( #12660, #60207, #56641, #282 ) ) ;
#28536=ORIENTED_EDGE ( 'NONE', *, *, #57118, .T. ) ;
#28538=CIRCLE ( 'NONE', #6062, 1.000000000000001554 ) ;
#28570=LINE ( 'NONE', #60580, #47717 ) ;
#28608=CARTESIAN_POINT ( 'NONE',  ( -48.30000751666425174, -13.25410963537987286, 0.9681788673137204926 ) ) ;
#28626=CARTESIAN_POINT ( 'NONE',  ( -54.93556801395976663, -8.762778093175661809, -2.499999999999995559 ) ) ;
#28648=EDGE_CURVE ( 'NONE', #17121, #51653, #29412, .T. ) ;
#28664=CARTESIAN_POINT ( 'NONE',  ( -57.33772693497696338, -7.785970543056433435, -0.9053205669554239554 ) ) ;
#28680=CARTESIAN_POINT ( 'NONE',  ( -58.75000000000000000, -13.99999999999999822, 18.10000000000000497 ) ) ;
#28717=CIRCLE ( 'NONE', #17519, 1.000000000000000000 ) ;
#28801=CARTESIAN_POINT ( 'NONE',  ( -52.24999999999999289, 4.336808689942018722E-16, -5.099999999999999645 ) ) ;
#28810=CARTESIAN_POINT ( 'NONE',  ( -29.83276705773152315, -8.499999999999996447, 0.3716419282406659419 ) ) ;
#28835=CARTESIAN_POINT ( 'NONE',  ( -29.91370621994235890, -7.761720733523295834, -0.7755720678495816589 ) ) ;
#28838=DIRECTION ( 'NONE',  ( -1.000000000000000000, 0.000000000000000000, 0.000000000000000000 ) ) ;
#28867=CARTESIAN_POINT ( 'NONE',  ( -28.74999999999999645, -8.499999999999996447, 18.10000000000000497 ) ) ;
#28869=CARTESIAN_POINT ( 'NONE',  ( -50.39495521537276090, -10.76536571987046820, 3.807206309028079882 ) ) ;
#28871=ORIENTED_EDGE ( 'NONE', *, *, #44225, .T. ) ;
#28881=CARTESIAN_POINT ( 'NONE',  ( -75.75000000000000000, -0.9999999999999995559, 19.00000000000000000 ) ) ;
#28890=CARTESIAN_POINT ( 'NONE',  ( -87.50000000000000000, -8.499999999999989342, 24.00000000000000000 ) ) ;
#28894=CARTESIAN_POINT ( 'NONE',  ( -52.24999999999999289, 4.336808689942018722E-16, -5.099999999999999645 ) ) ;
#28909=( BOUNDED_SURFACE ( )  B_SPLINE_SURFACE ( 3, 2, ( 
 ( #53909, #17363, #60243 ),
 ( #65867, #1787, #37807 ),
 ( #17003, #5713, #43081 ),
 ( #38493, #48694, #33500 ) ),
 .UNSPECIFIED., .F., .F., .F. ) 
 B_SPLINE_SURFACE_WITH_KNOTS ( ( 4, 4 ),
 ( 3, 3 ),
 ( 1.868947704930512543E-15, 0.002371732043463299026 ),
 ( 0.000000000000000000, 1.000000000000000000 ),
 .UNSPECIFIED. ) 
 GEOMETRIC_REPRESENTATION_ITEM ( )  RATIONAL_B_SPLINE_SURFACE ( (
 ( 1.000000000000000000, 0.9473232638934960814, 1.000000000000000000),
 ( 1.000000000000000000, 0.9785952379402158563, 1.000000000000000000),
 ( 1.000000000000000000, 1.000279878396717725, 1.000000000000000000),
 ( 1.000000000000000000, 1.000000000000000000, 1.000000000000000000) ) ) 
 REPRESENTATION_ITEM ( '' )  SURFACE ( )  );
#28942=CARTESIAN_POINT ( 'NONE',  ( -50.11702274195462792, -10.88632520110945734, 3.736191679969255386 ) ) ;
#29037=DIRECTION ( 'NONE',  ( 1.000000000000000000, 0.000000000000000000, 0.000000000000000000 ) ) ;
#29126=AXIS2_PLACEMENT_3D ( 'NONE', #68034, #41308, #14916 ) ;
#29127=CARTESIAN_POINT ( 'NONE',  ( -31.24124550007784507, -8.558011161593890748, -0.5650761621075199859 ) ) ;
#29145=EDGE_CURVE ( 'NONE', #17716, #40317, #43662, .T. ) ;
#29174=AXIS2_PLACEMENT_3D ( 'NONE', #32039, #47939, #26404 ) ;
#29187=VECTOR ( 'NONE', #1686, 1000.000000000000000 ) ;
#29221=EDGE_CURVE ( 'NONE', #35999, #62163, #8057, .T. ) ;
#29223=DIRECTION ( 'NONE',  ( -1.000000000000000000, 0.000000000000000000, 0.000000000000000000 ) ) ;
#29255=( GEOMETRIC_REPRESENTATION_CONTEXT ( 3 ) GLOBAL_UNCERTAINTY_ASSIGNED_CONTEXT ( ( #41951 ) ) GLOBAL_UNIT_ASSIGNED_CONTEXT ( ( #48360, #5380, #31788 ) ) REPRESENTATION_CONTEXT ( 'NONE', 'WORKASPACE' ) );
#29272=ORIENTED_EDGE ( 'NONE', *, *, #28474, .T. ) ;
#29337=( BOUNDED_SURFACE ( )  B_SPLINE_SURFACE ( 3, 2, ( 
 ( #44281, #29424, #40034 ),
 ( #6937, #55475, #55818 ),
 ( #6568, #12905, #34697 ),
 ( #56155, #49524, #1252 ),
 ( #1936, #17528, #38998 ),
 ( #60391, #61094, #44960 ),
 ( #12195, #33668, #23136 ),
 ( #7980, #55110, #34370 ),
 ( #1608, #50896, #45659 ),
 ( #28362, #44626, #66022 ),
 ( #9030, #30813, #47397 ),
 ( #56506, #52313, #46716 ) ),
 .UNSPECIFIED., .F., .F., .F. ) 
 B_SPLINE_SURFACE_WITH_KNOTS ( ( 4, 2, 2, 2, 2, 4 ),
 ( 3, 3 ),
 ( -8.673617379884035472E-18, 0.001550269635854629969, 0.002325404453781949182, 0.003100539271709268612, 0.004650808907563907038, 0.006201078543418545898 ),
 ( 0.000000000000000000, 1.000000000000000000 ),
 .UNSPECIFIED. ) 
 GEOMETRIC_REPRESENTATION_ITEM ( )  RATIONAL_B_SPLINE_SURFACE ( (
 ( 1.000000000000000000, 0.8674236696762899212, 1.000000000000000000),
 ( 1.000000000000000000, 0.8645660010316111865, 1.000000000000000000),
 ( 1.000000000000000000, 0.8607579482992175901, 1.000000000000000000),
 ( 1.000000000000000000, 0.8539431028568349458, 1.000000000000000000),
 ( 1.000000000000000000, 0.8514892559288537166, 1.000000000000000000),
 ( 1.000000000000000000, 0.8463012804488235785, 1.000000000000000000),
 ( 1.000000000000000000, 0.8435608369020011210, 1.000000000000000000),
 ( 1.000000000000000000, 0.8352445106661940954, 1.000000000000000000),
 ( 1.000000000000000000, 0.8295255392545153317, 1.000000000000000000),
 ( 1.000000000000000000, 0.8186818959322059719, 1.000000000000000000),
 ( 1.000000000000000000, 0.8135412794198538800, 1.000000000000000000),
 ( 1.000000000000000000, 0.8093049424017615401, 1.000000000000000000) ) ) 
 REPRESENTATION_ITEM ( '' )  SURFACE ( )  );
#29355=CARTESIAN_POINT ( 'NONE',  ( -16.75000000000000000, -3.000000000000000000, 20.00000000000000000 ) ) ;
#29365=CARTESIAN_POINT ( 'NONE',  ( -25.21060798583054563, 4.336808689942018722E-16, 0.000000000000000000 ) ) ;
#29406=ORIENTED_EDGE ( 'NONE', *, *, #54395, .F. ) ;
#29412=CIRCLE ( 'NONE', #68758, 5.000000000000000000 ) ;
#29424=CARTESIAN_POINT ( 'NONE',  ( -34.48878133304234694, -10.53184416402257106, 3.891476709836707126 ) ) ;
#29447=EDGE_CURVE ( 'NONE', #20404, #41337, #21489, .T. ) ;
#29467=VERTEX_POINT ( 'NONE', #7043 ) ;
#29494=LINE ( 'NONE', #14720, #24887 ) ;
#29517=CARTESIAN_POINT ( 'NONE',  ( -30.38025804287905629, -8.499999999999996447, 0.06931351858119244591 ) ) ;
#29526=ORIENTED_EDGE ( 'NONE', *, *, #25869, .F. ) ;
#29544=DIRECTION ( 'NONE',  ( 1.000000000000000000, 0.000000000000000000, 0.000000000000000000 ) ) ;
#29573=VERTEX_POINT ( 'NONE', #40819 ) ;
#29575=ORIENTED_EDGE ( 'NONE', *, *, #651, .T. ) ;
#29625=CARTESIAN_POINT ( 'NONE',  ( -12.74999999999999822, -0.9999999999999995559, 6.000000000000001776 ) ) ;
#29700=CARTESIAN_POINT ( 'NONE',  ( -71.75000000000000000, -3.000000000000000000, 20.00000000000000000 ) ) ;
#29731=VECTOR ( 'NONE', #25253, 1000.000000000000000 ) ;
#29768=PLANE ( 'NONE',  #13380 ) ;
#29807=ORIENTED_EDGE ( 'NONE', *, *, #41330, .F. ) ;
#29824=CARTESIAN_POINT ( 'NONE',  ( -11.74999999999999645, -3.585786437626905077, 19.00000000000000000 ) ) ;
#29847=VERTEX_POINT ( 'NONE', #23826 ) ;
#29856=DIRECTION ( 'NONE',  ( -1.000000000000000000, 0.000000000000000000, 0.000000000000000000 ) ) ;
#29896=DIRECTION ( 'NONE',  ( 0.000000000000000000, 0.000000000000000000, 1.000000000000000000 ) ) ;
#29911=ORIENTED_EDGE ( 'NONE', *, *, #14381, .F. ) ;
#29920=LINE ( 'NONE', #51378, #26487 ) ;
#29931=CARTESIAN_POINT ( 'NONE',  ( -56.30661091817325570, -8.499999999999996447, 7.186868961046329218 ) ) ;
#29968=CARTESIAN_POINT ( 'NONE',  ( -43.75000000000000000, 0.000000000000000000, -6.999999999999999112 ) ) ;
#30115=FACE_OUTER_BOUND ( 'NONE', #1520, .T. ) ;
#30117=EDGE_CURVE ( 'NONE', #14523, #31107, #28570, .T. ) ;
#30133=ORIENTED_EDGE ( 'NONE', *, *, #58358, .F. ) ;
#30151=CARTESIAN_POINT ( 'NONE',  ( -53.32003218646550380, -10.00128081186071327, -3.271960291195576076 ) ) ;
#30177=DIRECTION ( 'NONE',  ( 0.000000000000000000, 0.000000000000000000, 1.000000000000000000 ) ) ;
#30204=CIRCLE ( 'NONE', #8892, 1.000000000000000888 ) ;
#30219=VERTEX_POINT ( 'NONE', #1453 ) ;
#30222=ORIENTED_EDGE ( 'NONE', *, *, #28474, .F. ) ;
#30231=VERTEX_POINT ( 'NONE', #22983 ) ;
#30234=AXIS2_PLACEMENT_3D ( 'NONE', #42376, #37450, #5354 ) ;
#30245=ADVANCED_FACE ( 'NONE', ( #47778 ), #42479, .F. ) ;
#30260=EDGE_CURVE ( 'NONE', #1406, #33970, #38706, .T. ) ;
#30263=ORIENTED_EDGE ( 'NONE', *, *, #61031, .F. ) ;
#30323=EDGE_LOOP ( 'NONE', ( #1646, #7888 ) ) ;
#30327=ORIENTED_EDGE ( 'NONE', *, *, #43064, .F. ) ;
#30328=DIRECTION ( 'NONE',  ( 0.000000000000000000, 1.000000000000000000, 0.000000000000000000 ) ) ;
#30330=DIRECTION ( 'NONE',  ( 0.7239014318309263674, -0.3935725838095961437, -0.5666280422522106397 ) ) ;
#30346=PLANE ( 'NONE',  #29126 ) ;
#30366=CARTESIAN_POINT ( 'NONE',  ( -15.75000000000000000, 4.336808689942018722E-16, 24.00000000000000000 ) ) ;
#30379=ADVANCED_FACE ( 'NONE', ( #40563 ), #4331, .T. ) ;
#30392=ORIENTED_EDGE ( 'NONE', *, *, #61100, .F. ) ;
#30461=EDGE_CURVE ( 'NONE', #59113, #63964, #27447, .T. ) ;
#30500=VECTOR ( 'NONE', #1501, 1000.000000000000000 ) ;
#30510=CARTESIAN_POINT ( 'NONE',  ( -70.75000000000000000, -0.9999999999999995559, 19.00000000000000000 ) ) ;
#30548=PLANE ( 'NONE',  #18033 ) ;
#30558=DIRECTION ( 'NONE',  ( -1.084202172485503448E-16, 1.000000000000000000, 0.000000000000000000 ) ) ;
#30562=( BOUNDED_CURVE ( )  B_SPLINE_CURVE ( 3, ( #16656, #43069, #10663, #64473 ),
 .UNSPECIFIED., .F., .F. ) 
 B_SPLINE_CURVE_WITH_KNOTS ( ( 4, 4 ),
 ( 3.931838538365183489, 4.712388980384689674 ),
 .UNSPECIFIED. ) 
 CURVE ( )  GEOMETRIC_REPRESENTATION_ITEM ( )  RATIONAL_B_SPLINE_CURVE ( ( 1.000000000000000000, 0.9498695926598449413, 0.9498695926598449413, 1.000000000000000000 ) ) 
 REPRESENTATION_ITEM ( '' )  );
#30569=EDGE_CURVE ( 'NONE', #20128, #41095, #44226, .T. ) ;
#30594=EDGE_CURVE ( 'NONE', #10826, #33018, #32937, .T. ) ;
#30609=CARTESIAN_POINT ( 'NONE',  ( -54.08341698273633824, -9.461864478049029969, 4.963675025618371706 ) ) ;
#30642=CARTESIAN_POINT ( 'NONE',  ( -3.000000000000000000, -3.499999999999999556, 24.00000000000000000 ) ) ;
#30686=DIRECTION ( 'NONE',  ( -0.000000000000000000, 1.000000000000000000, 0.000000000000000000 ) ) ;
#30721=AXIS2_PLACEMENT_3D ( 'NONE', #59639, #64915, #11459 ) ;
#30734=EDGE_CURVE ( 'NONE', #51601, #24199, #69273, .T. ) ;
#30765=CARTESIAN_POINT ( 'NONE',  ( -59.35479220832651492, -7.603157425156885196, -0.1359663579351287899 ) ) ;
#30813=CARTESIAN_POINT ( 'NONE',  ( -39.62710692636852627, -13.39358289589475071, 2.720715303612538882 ) ) ;
#30841=LINE ( 'NONE', #31175, #48921 ) ;
#30939=CARTESIAN_POINT ( 'NONE',  ( -15.75000000000000000, -3.000000000000000000, 18.00000000000000000 ) ) ;
#30952=ORIENTED_EDGE ( 'NONE', *, *, #26819, .F. ) ;
#31012=CARTESIAN_POINT ( 'NONE',  ( -60.16623008473946044, -7.538574111777714748, -8.332478740366983261E-17 ) ) ;
#31013=VERTEX_POINT ( 'NONE', #34043 ) ;
#31018=ORIENTED_EDGE ( 'NONE', *, *, #9466, .F. ) ;
#31078=CARTESIAN_POINT ( 'NONE',  ( -3.000000000000000000, -3.499999999999999556, 24.00000000000000000 ) ) ;
#31079=CYLINDRICAL_SURFACE ( 'NONE', #44, 3.100000000000003642 ) ;
#31080=CARTESIAN_POINT ( 'NONE',  ( -54.23088132574830666, -9.395153247374610217, -2.525443637521251006 ) ) ;
#31087=SURFACE_SIDE_STYLE ('',( #15639 ) ) ;
#31094=ORIENTED_EDGE ( 'NONE', *, *, #8840, .T. ) ;
#31104=LINE ( 'NONE', #10380, #41122 ) ;
#31105=DIRECTION ( 'NONE',  ( 0.000000000000000000, 0.000000000000000000, -1.000000000000000000 ) ) ;
#31107=VERTEX_POINT ( 'NONE', #46549 ) ;
#31142=DIRECTION ( 'NONE',  ( 1.000000000000000000, 0.000000000000000000, 0.000000000000000000 ) ) ;
#31162=CARTESIAN_POINT ( 'NONE',  ( -27.34027958857958396, -7.539040513630480334, -3.506716401632803404E-16 ) ) ;
#31167=CARTESIAN_POINT ( 'NONE',  ( -83.49999999999998579, -3.499999999999999556, 24.00000000000000000 ) ) ;
#31175=CARTESIAN_POINT ( 'NONE',  ( -74.75000000000000000, -4.000000000000000000, 0.000000000000000000 ) ) ;
#31199=( NAMED_UNIT ( * ) SI_UNIT ( $, .STERADIAN. ) SOLID_ANGLE_UNIT ( ) );
#31201=CARTESIAN_POINT ( 'NONE',  ( -32.02323290426848956, -8.704246530741336585, 6.357025138609439630 ) ) ;
#31313=DIRECTION ( 'NONE',  ( 0.000000000000000000, 0.000000000000000000, -1.000000000000000000 ) ) ;
#31321=B_SPLINE_CURVE_WITH_KNOTS ( 'NONE', 3,
 ( #19138, #19494, #45915, #57485, #8615, #2583 ),
 .UNSPECIFIED., .F., .F.,
 ( 4, 2, 4 ),
 ( 0.000000000000000000, 0.0007817461686317332984, 0.001563492337263466597 ),
 .UNSPECIFIED. ) ;
#31362=EDGE_CURVE ( 'NONE', #43417, #46008, #42079, .T. ) ;
#31387=ORIENTED_EDGE ( 'NONE', *, *, #17873, .T. ) ;
#31413=( NAMED_UNIT ( * ) SI_UNIT ( $, .STERADIAN. ) SOLID_ANGLE_UNIT ( ) );
#31427=AXIS2_PLACEMENT_3D ( 'NONE', #5617, #27069, #298 ) ;
#31439=LINE ( 'NONE', #62757, #23685 ) ;
#31447=CARTESIAN_POINT ( 'NONE',  ( -36.12863118297439513, -11.74752507246378386, 1.561659418384358400 ) ) ;
#31451=CARTESIAN_POINT ( 'NONE',  ( -57.58629378005873889, -7.761720733523185700, -0.7755720678490086728 ) ) ;
#31459=DIRECTION ( 'NONE',  ( 0.000000000000000000, 0.000000000000000000, -1.000000000000000000 ) ) ;
#31486=LINE ( 'NONE', #26214, #5400 ) ;
#31559=CARTESIAN_POINT ( 'NONE',  ( -34.27411267550463236, -10.24482008810693578, 4.106145367377594724 ) ) ;
#31618=AXIS2_PLACEMENT_3D ( 'NONE', #67794, #19592, #9411 ) ;
#31630=CARTESIAN_POINT ( 'NONE',  ( -57.74999999999999289, 0.000000000000000000, -7.000000000000000000 ) ) ;
#31639=ORIENTED_EDGE ( 'NONE', *, *, #1983, .T. ) ;
#31679=CARTESIAN_POINT ( 'NONE',  ( -26.79538245034556709, -7.499999999999997335, 1.000000000000000000 ) ) ;
#31703=ADVANCED_FACE ( 'NONE', ( #42225 ), #20352, .F. ) ;
#31710=ORIENTED_EDGE ( 'NONE', *, *, #38638, .F. ) ;
#31750=ORIENTED_EDGE ( 'NONE', *, *, #9965, .T. ) ;
#31765=EDGE_CURVE ( 'NONE', #22278, #30219, #24934, .T. ) ;
#31788=( NAMED_UNIT ( * ) SI_UNIT ( $, .STERADIAN. ) SOLID_ANGLE_UNIT ( ) );
#31793=DIRECTION ( 'NONE',  ( 1.000000000000000000, 0.000000000000000000, 0.000000000000000000 ) ) ;
#31802=CARTESIAN_POINT ( 'NONE',  ( -83.49999999999998579, -2.499999999999999556, 0.000000000000000000 ) ) ;
#31806=CARTESIAN_POINT ( 'NONE',  ( -76.16421356237310647, 3.244476573706588632E-16, 19.41421356237309581 ) ) ;
#31808=AXIS2_PLACEMENT_3D ( 'NONE', #44341, #17584, #27039 ) ;
#31816=DIRECTION ( 'NONE',  ( -1.000000000000000000, 0.000000000000000000, 0.000000000000000000 ) ) ;
#31821=EDGE_LOOP ( 'NONE', ( #60932, #55859, #18710, #44440, #58224, #31094 ) ) ;
#31832=ORIENTED_EDGE ( 'NONE', *, *, #66785, .F. ) ;
#31853=DIRECTION ( 'NONE',  ( -0.000000000000000000, -0.000000000000000000, 1.000000000000000000 ) ) ;
#31875=VECTOR ( 'NONE', #36825, 1000.000000000000000 ) ;
#31907=VECTOR ( 'NONE', #32588, 1000.000000000000000 ) ;
#31912=EDGE_CURVE ( 'NONE', #20367, #737, #15203, .T. ) ;
#31918=ORIENTED_EDGE ( 'NONE', *, *, #49723, .F. ) ;
#31978=DIRECTION ( 'NONE',  ( 1.000000000000000000, 7.703719777548942317E-32, 0.000000000000000000 ) ) ;
#31993=CARTESIAN_POINT ( 'NONE',  ( -76.75000000000000000, -0.9999999999999995559, 7.000000000000001776 ) ) ;
#31999=DIRECTION ( 'NONE',  ( -1.000000000000000000, 0.000000000000000000, 0.000000000000000000 ) ) ;
#32021=CARTESIAN_POINT ( 'NONE',  ( -30.10526806553660606, -8.499999999999996447, 0.2211649376128430600 ) ) ;
#32039=CARTESIAN_POINT ( 'NONE',  ( -12.74999999999999822, 4.336808689942017736E-16, 7.000000000000001776 ) ) ;
#32052=CYLINDRICAL_SURFACE ( 'NONE', #40621, 1.000000000000000000 ) ;
#32076=ORIENTED_EDGE ( 'NONE', *, *, #30260, .F. ) ;
#32090=CARTESIAN_POINT ( 'NONE',  ( -4.000000000000000000, 4.336808689942018722E-16, -0.000000000000000000 ) ) ;
#32097=APPLICATION_CONTEXT ( 'automotive_design' ) ;
#32123=TOROIDAL_SURFACE ( 'NONE', #1738, 8.999999999999998224, 5.000000000000000000 ) ;
#32160=ADVANCED_FACE ( 'NONE', ( #30115 ), #51592, .F. ) ;
#32203=VECTOR ( 'NONE', #69380, 1000.000000000000000 ) ;
#32206=SPHERICAL_SURFACE ( 'NONE', #23528, 1.000000000000000000 ) ;
#32208=DIRECTION ( 'NONE',  ( -0.000000000000000000, 1.000000000000000000, -0.000000000000000000 ) ) ;
#32236=EDGE_CURVE ( 'NONE', #63964, #38572, #9748, .T. ) ;
#32256=ORIENTED_EDGE ( 'NONE', *, *, #63135, .F. ) ;
#32327=VERTEX_POINT ( 'NONE', #1874 ) ;
#32333=DIRECTION ( 'NONE',  ( 0.000000000000000000, 0.000000000000000000, -1.000000000000000000 ) ) ;
#32334=ORIENTED_EDGE ( 'NONE', *, *, #61347, .T. ) ;
#32338=DIRECTION ( 'NONE',  ( 0.000000000000000000, -0.000000000000000000, 1.000000000000000000 ) ) ;
#32391=CARTESIAN_POINT ( 'NONE',  ( -57.11117894258828898, -7.808072229298645084, -1.023575524669360748 ) ) ;
#32403=CARTESIAN_POINT ( 'NONE',  ( -55.11713571482079033, -8.499999999999996447, 6.664929171799898633 ) ) ;
#32418=ORIENTED_EDGE ( 'NONE', *, *, #35095, .F. ) ;
#32434=DIRECTION ( 'NONE',  ( -0.000000000000000000, 1.000000000000000000, -0.000000000000000000 ) ) ;
#32471=EDGE_CURVE ( 'NONE', #2398, #32974, #62043, .T. ) ;
#32486=DIRECTION ( 'NONE',  ( -1.000000000000000000, -0.000000000000000000, -0.000000000000000000 ) ) ;
#32528=VERTEX_POINT ( 'NONE', #30366 ) ;
#32550=CARTESIAN_POINT ( 'NONE',  ( -71.75000000000000000, -0.9999999999999995559, 20.00000000000000000 ) ) ;
#32552=DIRECTION ( 'NONE',  ( 0.000000000000000000, 0.000000000000000000, 1.000000000000000000 ) ) ;
#32575=ORIENTED_EDGE ( 'NONE', *, *, #10119, .F. ) ;
#32588=DIRECTION ( 'NONE',  ( 1.000000000000000000, -1.189524669241239115E-16, -0.000000000000000000 ) ) ;
#32650=ORIENTED_EDGE ( 'NONE', *, *, #66891, .F. ) ;
#32670=B_SPLINE_CURVE_WITH_KNOTS ( 'NONE', 3,
 ( #50481, #12478, #49794, #33940, #23736, #66662, #54697, #12834, #17458, #27942, #38927, #55401 ),
 .UNSPECIFIED., .F., .F.,
 ( 4, 2, 2, 2, 2, 4 ),
 ( 0.000000000000000000, 0.001808836200486184593, 0.003617672400972369185, 0.004522090501215460072, 0.005426508601458550525, 0.007235344801944751381 ),
 .UNSPECIFIED. ) ;
#32689=CARTESIAN_POINT ( 'NONE',  ( -42.59457610709575448, -13.96731970680246171, 0.7787128058468592018 ) ) ;
#32697=ORIENTED_EDGE ( 'NONE', *, *, #69129, .T. ) ;
#32747=VERTEX_POINT ( 'NONE', #12381 ) ;
#32780=CARTESIAN_POINT ( 'NONE',  ( -33.39016983555134033, -9.443832887535089426, -2.000000000000000000 ) ) ;
#32816=ADVANCED_FACE ( 'NONE', ( #12044 ), #6766, .F. ) ;
#32823=EDGE_CURVE ( 'NONE', #53539, #45684, #66565, .T. ) ;
#32825=CARTESIAN_POINT ( 'NONE',  ( -41.40296580814450778, -13.81618002571821613, 2.682162060699885497 ) ) ;
#32828=DIRECTION ( 'NONE',  ( 1.000000000000000000, -1.445602896647339656E-16, 0.000000000000000000 ) ) ;
#32854=AXIS2_PLACEMENT_3D ( 'NONE', #3951, #30328, #20857 ) ;
#32858=CARTESIAN_POINT ( 'NONE',  ( -57.74999999999999289, 0.000000000000000000, -7.000000000000000000 ) ) ;
#32937=CIRCLE ( 'NONE', #53182, 1.000000000000000888 ) ;
#32965=CARTESIAN_POINT ( 'NONE',  ( -16.75000000000000000, -0.9999999999999995559, 24.00000000000000000 ) ) ;
#32967=CARTESIAN_POINT ( 'NONE',  ( -30.38025804287906695, -8.500000000000000000, 7.999999999999979572 ) ) ;
#32974=VERTEX_POINT ( 'NONE', #30642 ) ;
#33018=VERTEX_POINT ( 'NONE', #19409 ) ;
#33041=CARTESIAN_POINT ( 'NONE',  ( -53.60138880980050402, -9.947368421755438561, -2.262137787255405819 ) ) ;
#33137=EDGE_CURVE ( 'NONE', #35896, #31107, #54441, .T. ) ;
#33166=FACE_OUTER_BOUND ( 'NONE', #66160, .T. ) ;
#33172=DIRECTION ( 'NONE',  ( 1.000000000000000000, -0.000000000000000000, -0.000000000000000000 ) ) ;
#33182=DIRECTION ( 'NONE',  ( -1.445602896647339656E-16, -1.000000000000000000, 0.000000000000000000 ) ) ;
#33226=EDGE_LOOP ( 'NONE', ( #49627, #17797, #57253, #15195, #12529, #43725, #50452 ) ) ;
#33368=VERTEX_POINT ( 'NONE', #52994 ) ;
#33446=ORIENTED_EDGE ( 'NONE', *, *, #66493, .F. ) ;
#33453=CARTESIAN_POINT ( 'NONE',  ( -57.58629378005873889, -7.761720733523186588, -0.7755720678490058972 ) ) ;
#33475=CARTESIAN_POINT ( 'NONE',  ( -34.31731514509471026, -10.02774732068182750, -3.508434557029131540 ) ) ;
#33478=UNCERTAINTY_MEASURE_WITH_UNIT (LENGTH_MEASURE( 1.000000000000000082E-05 ), #68518, 'distance_accuracy_value', 'NONE');
#33500=CARTESIAN_POINT ( 'NONE',  ( -34.31243252642629926, -10.02680648607947589, -3.499999999999429345 ) ) ;
#33514=FACE_OUTER_BOUND ( 'NONE', #46224, .T. ) ;
#33548=CARTESIAN_POINT ( 'NONE',  ( -83.49999999999998579, -3.499999999999999556, 0.000000000000000000 ) ) ;
#33559=ORIENTED_EDGE ( 'NONE', *, *, #36089, .T. ) ;
#33668=CARTESIAN_POINT ( 'NONE',  ( -36.73960380223706323, -12.13027782366804708, 3.018653417519900906 ) ) ;
#33670=ADVANCED_FACE ( 'NONE', ( #54622 ), #21262, .T. ) ;
#33700=CARTESIAN_POINT ( 'NONE',  ( -11.99999999999999822, -6.499999999999999112, 21.00000000000000000 ) ) ;
#33760=LINE ( 'NONE', #34111, #50801 ) ;
#33778=AXIS2_PLACEMENT_3D ( 'NONE', #40643, #67703, #57129 ) ;
#33788=CARTESIAN_POINT ( 'NONE',  ( -55.66437634316022098, -8.712199461619613672, -1.102180370744095139 ) ) ;
#33795=ORIENTED_EDGE ( 'NONE', *, *, #37565, .T. ) ;
#33818=ORIENTED_EDGE ( 'NONE', *, *, #53533, .T. ) ;
#33824=DIRECTION ( 'NONE',  ( 1.000000000000000000, -0.000000000000000000, -0.000000000000000000 ) ) ;
#33842=CIRCLE ( 'NONE', #67554, 1.000000000000000888 ) ;
#33889=CARTESIAN_POINT ( 'NONE',  ( -48.87409065588625623, -13.04242605562483703, 1.033469574933718604 ) ) ;
#33936=CARTESIAN_POINT ( 'NONE',  ( -54.73148258177910463, -9.107254030097815090, -2.000000000000000000 ) ) ;
#33940=CARTESIAN_POINT ( 'NONE',  ( -49.94031648296357417, -12.57106785925259551, 1.201245605581311882 ) ) ;
#33961=PLANE ( 'NONE',  #1718 ) ;
#33970=VERTEX_POINT ( 'NONE', #45517 ) ;
#33989=DIRECTION ( 'NONE',  ( -0.000000000000000000, -0.000000000000000000, 1.000000000000000000 ) ) ;
#34043=CARTESIAN_POINT ( 'NONE',  ( -12.74999999999999822, 4.336808689942018722E-16, 5.000000000000001776 ) ) ;
#34055=CARTESIAN_POINT ( 'NONE',  ( -17.75000000000000355, -3.000000000000000000, 20.00000000000000000 ) ) ;
#34060=DIRECTION ( 'NONE',  ( 0.000000000000000000, 0.000000000000000000, 1.000000000000000000 ) ) ;
#34084=ORIENTED_EDGE ( 'NONE', *, *, #14463, .T. ) ;
#34090=ORIENTED_EDGE ( 'NONE', *, *, #12000, .F. ) ;
#34103=CARTESIAN_POINT ( 'NONE',  ( -60.39042638714564504, -8.499999999999994671, 1.000000000000000000 ) ) ;
#34111=CARTESIAN_POINT ( 'NONE',  ( 3.851859888774471706E-31, -8.500000000000000000, 24.00000000000000000 ) ) ;
#34124=EDGE_LOOP ( 'NONE', ( #60589, #24677, #5093, #33818 ) ) ;
#34168=ORIENTED_EDGE ( 'NONE', *, *, #30117, .T. ) ;
#34203=VECTOR ( 'NONE', #34278, 1000.000000000000000 ) ;
#34210=DIRECTION ( 'NONE',  ( -0.000000000000000000, -0.000000000000000000, -1.000000000000000000 ) ) ;
#34278=DIRECTION ( 'NONE',  ( -0.000000000000000000, 1.000000000000000000, -0.000000000000000000 ) ) ;
#34281=CARTESIAN_POINT ( 'NONE',  ( -36.37589283219813296, -10.39236702006417268, 4.075234830157013377 ) ) ;
#34370=CARTESIAN_POINT ( 'NONE',  ( -37.13402269541712286, -12.35322054092467425, 1.284749433650013373 ) ) ;
#34387=ORIENTED_EDGE ( 'NONE', *, *, #49723, .T. ) ;
#34425=LINE ( 'NONE', #44683, #134 ) ;
#34506=EDGE_LOOP ( 'NONE', ( #43358, #29406, #8782, #25082 ) ) ;
#34507=CARTESIAN_POINT ( 'NONE',  ( -37.74999999999999289, 0.000000000000000000, -5.100000000000000533 ) ) ;
#34584=VERTEX_POINT ( 'NONE', #11895 ) ;
#34603=DIRECTION ( 'NONE',  ( 0.000000000000000000, 1.000000000000000000, 0.000000000000000000 ) ) ;
#34625=EDGE_CURVE ( 'NONE', #63373, #54365, #31439, .T. ) ;
#34660=ORIENTED_EDGE ( 'NONE', *, *, #26819, .T. ) ;
#34681=ORIENTED_EDGE ( 'NONE', *, *, #25746, .F. ) ;
#34697=CARTESIAN_POINT ( 'NONE',  ( -34.68069995552857421, -10.68067889009693872, 2.165721509536973954 ) ) ;
#34717=LINE ( 'NONE', #64762, #7981 ) ;
#34763=ORIENTED_EDGE ( 'NONE', *, *, #462, .T. ) ;
#34764=ORIENTED_EDGE ( 'NONE', *, *, #26578, .F. ) ;
#34766=CARTESIAN_POINT ( 'NONE',  ( -30.83411394072454925, -7.922994316747240084, -1.304230133214211662 ) ) ;
#34789=CIRCLE ( 'NONE', #66212, 3.100000000000001865 ) ;
#34809=ORIENTED_EDGE ( 'NONE', *, *, #45868, .F. ) ;
#34812=DIRECTION ( 'NONE',  ( -0.000000000000000000, 1.000000000000000000, 0.000000000000000000 ) ) ;
#34832=ORIENTED_EDGE ( 'NONE', *, *, #57503, .F. ) ;
#34843=DIRECTION ( 'NONE',  ( 0.000000000000000000, 1.000000000000000000, 0.000000000000000000 ) ) ;
#34847=EDGE_LOOP ( 'NONE', ( #12018, #21311, #30327, #19432 ) ) ;
#34878=DIRECTION ( 'NONE',  ( 0.000000000000000000, 1.000000000000000000, 0.000000000000000000 ) ) ;
#34941=VECTOR ( 'NONE', #224, 1000.000000000000000 ) ;
#34946=CARTESIAN_POINT ( 'NONE',  ( -51.54855153546065338, -10.14125325047201187, 4.285873052701354879 ) ) ;
#34966=EDGE_CURVE ( 'NONE', #10826, #63373, #51527, .T. ) ;
#35005=VECTOR ( 'NONE', #8734, 1000.000000000000000 ) ;
#35043=CIRCLE ( 'NONE', #24944, 6.000000000000005329 ) ;
#35069=DIRECTION ( 'NONE',  ( 0.000000000000000000, 1.000000000000000000, -0.000000000000000000 ) ) ;
#35095=EDGE_CURVE ( 'NONE', #51912, #23284, #6224, .T. ) ;
#35104=CARTESIAN_POINT ( 'NONE',  ( -54.07000006678288884, -9.448433432976491630, -2.594157102514922375 ) ) ;
#35128=CARTESIAN_POINT ( 'NONE',  ( -32.13196390538205094, -8.494561555450525603, -2.203021938113412848 ) ) ;
#35138=DIRECTION ( 'NONE',  ( -0.000000000000000000, -0.000000000000000000, 1.000000000000000000 ) ) ;
#35180=EDGE_CURVE ( 'NONE', #26367, #48229, #21597, .T. ) ;
#35193=LINE ( 'NONE', #56651, #17098 ) ;
#35217=CARTESIAN_POINT ( 'NONE',  ( -54.08595089178545123, -9.512283121613346992, 3.449313401996987327 ) ) ;
#35401=CARTESIAN_POINT ( 'NONE',  ( -83.49999999999998579, 4.336808689942018722E-16, 24.00000000000000000 ) ) ;
#35434=DIRECTION ( 'NONE',  ( 1.000000000000000000, -1.189524669241239115E-16, -0.000000000000000000 ) ) ;
#35450=ORIENTED_EDGE ( 'NONE', *, *, #359, .F. ) ;
#35484=CARTESIAN_POINT ( 'NONE',  ( -32.56443198604022626, -8.762778093175665362, -2.499999999999996891 ) ) ;
#35496=CIRCLE ( 'NONE', #61334, 1.000000000000000888 ) ;
#35514=ADVANCED_FACE ( 'NONE', ( #44665 ), #28407, .T. ) ;
#35520=DIRECTION ( 'NONE',  ( 0.9544448354272550006, -0.2817348470284508077, -0.09828800586081520851 ) ) ;
#35548=DIRECTION ( 'NONE',  ( -1.189524669241239115E-16, -1.000000000000000000, -0.000000000000000000 ) ) ;
#35562=EDGE_LOOP ( 'NONE', ( #65914, #29807, #53805, #56913 ) ) ;
#35573=DIRECTION ( 'NONE',  ( 1.000000000000000000, 0.000000000000000000, 0.000000000000000000 ) ) ;
#35631=EDGE_LOOP ( 'NONE', ( #32697, #36417, #18877, #63388 ) ) ;
#35635=ORIENTED_EDGE ( 'NONE', *, *, #66373, .T. ) ;
#35651=ORIENTED_EDGE ( 'NONE', *, *, #850, .F. ) ;
#35689=EDGE_CURVE ( 'NONE', #62302, #21323, #11743, .T. ) ;
#35697=CARTESIAN_POINT ( 'NONE',  ( -11.99999999999999822, -6.499999999999999112, 21.00000000000000000 ) ) ;
#35729=VECTOR ( 'NONE', #3313, 1000.000000000000000 ) ;
#35730=LINE ( 'NONE', #45955, #37083 ) ;
#35766=DIRECTION ( 'NONE',  ( 1.000000000000000000, 0.000000000000000000, 0.000000000000000000 ) ) ;
#35854=FACE_OUTER_BOUND ( 'NONE', #9851, .T. ) ;
#35859=AXIS2_PLACEMENT_3D ( 'NONE', #68222, #35520, #58023 ) ;
#35873=ORIENTED_EDGE ( 'NONE', *, *, #24223, .F. ) ;
#35896=VERTEX_POINT ( 'NONE', #4277 ) ;
#35930=DIRECTION ( 'NONE',  ( -0.000000000000000000, 1.000000000000000000, 0.000000000000000000 ) ) ;
#35964=CARTESIAN_POINT ( 'NONE',  ( -59.62102754835381546, -7.580807888618323886, -0.06943374021246458139 ) ) ;
#35991=CIRCLE ( 'NONE', #19134, 1.000000000000000888 ) ;
#35998=AXIS2_PLACEMENT_3D ( 'NONE', #56609, #47132, #18949 ) ;
#35999=VERTEX_POINT ( 'NONE', #18690 ) ;
#36042=AXIS2_PLACEMENT_3D ( 'NONE', #24488, #63100, #58516 ) ;
#36051=FACE_OUTER_BOUND ( 'NONE', #60129, .T. ) ;
#36063=DIRECTION ( 'NONE',  ( 1.000000000000000000, 0.000000000000000000, 0.000000000000000000 ) ) ;
#36086=ORIENTED_EDGE ( 'NONE', *, *, #11480, .T. ) ;
#36089=EDGE_CURVE ( 'NONE', #54598, #11986, #51446, .T. ) ;
#36135=EDGE_CURVE ( 'NONE', #23192, #19551, #2808, .T. ) ;
#36200=VERTEX_POINT ( 'NONE', #20773 ) ;
#36228=FACE_OUTER_BOUND ( 'NONE', #335, .T. ) ;
#36244=FACE_BOUND ( 'NONE', #39467, .T. ) ;
#36245=CARTESIAN_POINT ( 'NONE',  ( -87.50000000000000000, -8.499999999999989342, 21.00000000000000000 ) ) ;
#36295=CARTESIAN_POINT ( 'NONE',  ( -53.01121866695764595, -10.53184416402257462, 3.891476709836703574 ) ) ;
#36311=CARTESIAN_POINT ( 'NONE',  ( -34.01388385445504525, -9.805546523439568674, -3.361664814432062887 ) ) ;
#36343=CARTESIAN_POINT ( 'NONE',  ( -57.66965831571685897, -8.499999999999992895, 0.3729812355688906789 ) ) ;
#36417=ORIENTED_EDGE ( 'NONE', *, *, #18298, .F. ) ;
#36418=CARTESIAN_POINT ( 'NONE',  ( -87.50000000000000000, -7.499999999999990230, 24.00000000000000000 ) ) ;
#36425=FACE_OUTER_BOUND ( 'NONE', #24960, .T. ) ;
#36449=ADVANCED_FACE ( 'NONE', ( #22142 ), #49231, .F. ) ;
#36559=LINE ( 'NONE', #30510, #35005 ) ;
#36561=ADVANCED_FACE ( 'NONE', ( #24534 ), #60786, .F. ) ;
#36571=DIRECTION ( 'NONE',  ( 0.000000000000000000, 0.000000000000000000, 1.000000000000000000 ) ) ;
#36586=CARTESIAN_POINT ( 'NONE',  ( -53.78504481823340200, -9.584004935223168431, -3.223153552129623733 ) ) ;
#36616=DIRECTION ( 'NONE',  ( 0.000000000000000000, 1.000000000000000000, 0.000000000000000000 ) ) ;
#36652=CARTESIAN_POINT ( 'NONE',  ( -53.48759684591490071, -9.962924773521274702, 4.367854888790892787 ) ) ;
#36681=ORIENTED_EDGE ( 'NONE', *, *, #13743, .F. ) ;
#36695=TOROIDAL_SURFACE ( 'NONE', #5048, 2.000000000000000000, 1.000000000000000000 ) ;
#36755=EDGE_CURVE ( 'NONE', #13126, #30231, #26615, .T. ) ;
#36786=ORIENTED_EDGE ( 'NONE', *, *, #3914, .T. ) ;
#36825=DIRECTION ( 'NONE',  ( 1.000000000000000000, -1.445602896647339656E-16, -0.000000000000000000 ) ) ;
#36847=DIRECTION ( 'NONE',  ( -1.000000000000000000, 0.000000000000000000, 0.000000000000000000 ) ) ;
#36885=CARTESIAN_POINT ( 'NONE',  ( -35.31117902378667850, -9.718525487688223663, 4.712719346061684966 ) ) ;
#36940=EDGE_CURVE ( 'NONE', #13277, #25360, #28538, .T. ) ;
#36956=LINE ( 'NONE', #31630, #45621 ) ;
#36982=ADVANCED_FACE ( 'NONE', ( #62788 ), #42442, .T. ) ;
#37001=DIRECTION ( 'NONE',  ( 0.000000000000000000, 0.000000000000000000, 1.000000000000000000 ) ) ;
#37024=DIRECTION ( 'NONE',  ( 1.000000000000000000, -0.000000000000000000, -0.000000000000000000 ) ) ;
#37083=VECTOR ( 'NONE', #45630, 1000.000000000000000 ) ;
#37108=VECTOR ( 'NONE', #40726, 1000.000000000000000 ) ;
#37112=CARTESIAN_POINT ( 'NONE',  ( -53.72233514740115368, -9.706441612173417610, -3.029717619416509411 ) ) ;
#37120=DIRECTION ( 'NONE',  ( 1.000000000000000000, 0.000000000000000000, 0.000000000000000000 ) ) ;
#37138=EDGE_CURVE ( 'NONE', #51653, #17133, #52234, .T. ) ;
#37146=CARTESIAN_POINT ( 'NONE',  ( -30.38025804287906340, -13.49999999999999822, -2.000000000000000000 ) ) ;
#37157=VECTOR ( 'NONE', #8780, 1000.000000000000000 ) ;
#37197=AXIS2_PLACEMENT_3D ( 'NONE', #26826, #43095, #37120 ) ;
#37198=FACE_OUTER_BOUND ( 'NONE', #16777, .T. ) ;
#37211=ORIENTED_EDGE ( 'NONE', *, *, #43497, .T. ) ;
#37250=CARTESIAN_POINT ( 'NONE',  ( -28.74999999999999645, -8.499999999999996447, 15.00000000000000178 ) ) ;
#37251=CARTESIAN_POINT ( 'NONE',  ( -47.00571487472603138, -11.85301361210301607, 3.279042910798483312 ) ) ;
#37260=DIRECTION ( 'NONE',  ( 1.000000000000000000, 0.000000000000000000, 0.000000000000000000 ) ) ;
#37261=CARTESIAN_POINT ( 'NONE',  ( -87.50000000000000000, -8.499999999999989342, 24.00000000000000000 ) ) ;
#37268=CARTESIAN_POINT ( 'NONE',  ( -40.70406133565712992, -11.89285714285713880, 3.265330863013266693 ) ) ;
#37387=CIRCLE ( 'NONE', #53064, 13.76969600708473074 ) ;
#37392=CARTESIAN_POINT ( 'NONE',  ( -58.01150860321133251, -8.499999999997220002, -0.3572867894539443201 ) ) ;
#37423=CARTESIAN_POINT ( 'NONE',  ( -75.50000000000000000, -8.499999999999991118, 3.000000000000000000 ) ) ;
#37450=DIRECTION ( 'NONE',  ( -0.000000000000000000, 0.000000000000000000, -1.000000000000000000 ) ) ;
#37498=CARTESIAN_POINT ( 'NONE',  ( -34.18098754654297267, -10.00147920973261861, -3.272174344843567173 ) ) ;
#37499=DIRECTION ( 'NONE',  ( 7.703719777548942317E-32, -1.000000000000000000, -0.000000000000000000 ) ) ;
#37565=EDGE_CURVE ( 'NONE', #48229, #34584, #31321, .T. ) ;
#37605=EDGE_LOOP ( 'NONE', ( #41892, #29911, #18307 ) ) ;
#37606=CARTESIAN_POINT ( 'NONE',  ( -28.74999999999999645, -4.000000000000000000, 15.00000000000000178 ) ) ;
#37613=DIRECTION ( 'NONE',  ( 0.000000000000000000, -0.000000000000000000, 1.000000000000000000 ) ) ;
#37637=EDGE_CURVE ( 'NONE', #39801, #48124, #56803, .T. ) ;
#37641=AXIS2_PLACEMENT_3D ( 'NONE', #6103, #43102, #31793 ) ;
#37657=ORIENTED_EDGE ( 'NONE', *, *, #30461, .T. ) ;
#37686=DIRECTION ( 'NONE',  ( -1.189524669241239855E-16, -1.000000000000000000, 0.000000000000000000 ) ) ;
#37714=DIRECTION ( 'NONE',  ( 1.000000000000000000, 0.000000000000000000, 0.000000000000000000 ) ) ;
#37715=ADVANCED_FACE ( 'NONE', ( #10353, #63793, #5054 ), #53927, .T. ) ;
#37732=DIRECTION ( 'NONE',  ( 1.000000000000000000, 1.084202172485503448E-16, 0.000000000000000000 ) ) ;
#37733=VECTOR ( 'NONE', #61381, 1000.000000000000000 ) ;
#37737=( BOUNDED_CURVE ( )  B_SPLINE_CURVE ( 3, ( #46397, #29824, #19952, #41115 ),
 .UNSPECIFIED., .F., .F. ) 
 B_SPLINE_CURVE_WITH_KNOTS ( ( 4, 4 ),
 ( 0.000000000000000000, 1.570796326794896558 ),
 .UNSPECIFIED. ) 
 CURVE ( )  GEOMETRIC_REPRESENTATION_ITEM ( )  RATIONAL_B_SPLINE_CURVE ( ( 1.000000000000000000, 0.8047378541243649375, 0.8047378541243649375, 1.000000000000000000 ) ) 
 REPRESENTATION_ITEM ( '' )  );
#37747=ORIENTED_EDGE ( 'NONE', *, *, #57503, .T. ) ;
#37758=ORIENTED_EDGE ( 'NONE', *, *, #34966, .F. ) ;
#37774=DIRECTION ( 'NONE',  ( -0.000000000000000000, -1.000000000000000000, -0.000000000000000000 ) ) ;
#37807=CARTESIAN_POINT ( 'NONE',  ( -33.12716783835527679, -9.131344072917100263, -2.873593582817198566 ) ) ;
#37813=CARTESIAN_POINT ( 'NONE',  ( -40.04190075645216496, -13.49999999999999822, 0.8979962945199001512 ) ) ;
#37823=DIRECTION ( 'NONE',  ( 0.000000000000000000, 0.000000000000000000, 1.000000000000000000 ) ) ;
#37841=TOROIDAL_SURFACE ( 'NONE', #69233, 2.000000000000000000, 1.000000000000000000 ) ;
#37852=CARTESIAN_POINT ( 'NONE',  ( -15.75000000000000000, -4.000000000000000000, 20.00000000000000000 ) ) ;
#37877=CARTESIAN_POINT ( 'NONE',  ( -60.70461754965443646, -8.499999999999992895, 1.000000000000000000 ) ) ;
#37956=LINE ( 'NONE', #10490, #67796 ) ;
#37974=CARTESIAN_POINT ( 'NONE',  ( -4.000000000000000000, -3.499999999999999556, 24.00000000000000000 ) ) ;
#37994=DIRECTION ( 'NONE',  ( 0.000000000000000000, 1.000000000000000000, 0.000000000000000000 ) ) ;
#38019=CARTESIAN_POINT ( 'NONE',  ( -40.04190075645215785, -13.49999999999999822, 0.8979962945199000401 ) ) ;
#38024=EDGE_LOOP ( 'NONE', ( #15331, #33795, #52127, #50865, #15920, #17589, #13367, #39074 ) ) ;
#38059=CARTESIAN_POINT ( 'NONE',  ( -16.75000000000000000, 4.336808689942018722E-16, 20.00000000000000000 ) ) ;
#38099=CARTESIAN_POINT ( 'NONE',  ( -33.89861118948983432, -9.947368421052630083, -2.000000000000000000 ) ) ;
#38145=CARTESIAN_POINT ( 'NONE',  ( -11.99999999999999822, -6.499999999999999112, 21.00000000000000000 ) ) ;
#38154=CARTESIAN_POINT ( 'NONE',  ( -75.50000000000000000, -6.499999999999992006, 3.000000000000000000 ) ) ;
#38161=ADVANCED_FACE ( 'NONE', ( #10941 ), #48267, .F. ) ;
#38170=CARTESIAN_POINT ( 'NONE',  ( -33.89861118948982721, -9.947368421052624754, -2.000000000000000000 ) ) ;
#38232=AXIS2_PLACEMENT_3D ( 'NONE', #11268, #653, #64396 ) ;
#38235=CARTESIAN_POINT ( 'NONE',  ( 0.000000000000000000, 0.000000000000000000, 0.000000000000000000 ) ) ;
#38247=STYLED_ITEM ( 'NONE', ( #45598 ), #52290 ) ;
#38336=ORIENTED_EDGE ( 'NONE', *, *, #19994, .F. ) ;
#38438=CARTESIAN_POINT ( 'NONE',  ( -56.25313552506686676, -8.558999539123545830, -0.5698282025367524817 ) ) ;
#38459=EDGE_LOOP ( 'NONE', ( #68841, #6217, #13829, #5014 ) ) ;
#38485=CIRCLE ( 'NONE', #41832, 4.999999999999997335 ) ;
#38493=CARTESIAN_POINT ( 'NONE',  ( -34.31243252642629926, -10.02680648607947589, -3.499999999999429789 ) ) ;
#38572=VERTEX_POINT ( 'NONE', #25633 ) ;
#38604=VERTEX_POINT ( 'NONE', #36245 ) ;
#38610=LINE ( 'NONE', #60009, #68185 ) ;
#38638=EDGE_CURVE ( 'NONE', #25839, #66384, #52750, .T. ) ;
#38706=CIRCLE ( 'NONE', #19573, 1.000000000000000888 ) ;
#38712=CARTESIAN_POINT ( 'NONE',  ( 0.000000000000000000, 0.000000000000000000, 24.00000000000000000 ) ) ;
#38735=CARTESIAN_POINT ( 'NONE',  ( -28.74999999999999645, -13.99999999999999822, 11.89999999999999858 ) ) ;
#38757=ORIENTED_EDGE ( 'NONE', *, *, #63470, .T. ) ;
#38758=ORIENTED_EDGE ( 'NONE', *, *, #58856, .T. ) ;
#38767=ORIENTED_EDGE ( 'NONE', *, *, #11006, .T. ) ;
#38771=ORIENTED_EDGE ( 'NONE', *, *, #18298, .T. ) ;
#38775=CARTESIAN_POINT ( 'NONE',  ( -57.11974195712093660, -8.499999999999992895, 0.06931351858119258469 ) ) ;
#38841=EDGE_CURVE ( 'NONE', #51117, #20590, #61185, .T. ) ;
#38853=DIRECTION ( 'NONE',  ( 1.000000000000000000, 0.000000000000000000, 0.000000000000000000 ) ) ;
#38883=EDGE_CURVE ( 'NONE', #60509, #54981, #63469, .T. ) ;
#38899=CARTESIAN_POINT ( 'NONE',  ( -54.25530022753511616, -9.366146071587957422, -2.498496607514901768 ) ) ;
#38927=CARTESIAN_POINT ( 'NONE',  ( -53.22985755524383222, -10.31531486637975803, 2.417283891829344888 ) ) ;
#38937=ORIENTED_EDGE ( 'NONE', *, *, #8917, .T. ) ;
#38998=CARTESIAN_POINT ( 'NONE',  ( -35.59516224449775024, -11.38366882999885554, 1.750067940178240411 ) ) ;
#39003=CARTESIAN_POINT ( 'NONE',  ( -12.74999999999999822, -3.000000000000000000, 7.000000000000001776 ) ) ;
#39020=ORIENTED_EDGE ( 'NONE', *, *, #26451, .F. ) ;
#39073=CARTESIAN_POINT ( 'NONE',  ( -52.24999999999999289, 4.336808689942018722E-16, 0.000000000000000000 ) ) ;
#39074=ORIENTED_EDGE ( 'NONE', *, *, #57553, .T. ) ;
#39076=CARTESIAN_POINT ( 'NONE',  ( -26.79538245034556709, -7.499999999999997335, 0.000000000000000000 ) ) ;
#39113=CARTESIAN_POINT ( 'NONE',  ( -4.000000000000000000, 4.336808689942018722E-16, 24.00000000000000000 ) ) ;
#39146=LINE ( 'NONE', #60535, #20882 ) ;
#39171=CARTESIAN_POINT ( 'NONE',  ( -41.74159630588923875, -12.05724898635192233, 3.212438452487503149 ) ) ;
#39173=DIRECTION ( 'NONE',  ( 1.000000000000000000, 0.000000000000000000, 0.000000000000000000 ) ) ;
#39180=CARTESIAN_POINT ( 'NONE',  ( -83.49999999999998579, 4.336808689942018722E-16, -0.000000000000000000 ) ) ;
#39194=AXIS2_PLACEMENT_3D ( 'NONE', #22060, #43564, #49158 ) ;
#39203=DIRECTION ( 'NONE',  ( 1.000000000000000000, -1.084202172485504434E-16, -0.000000000000000000 ) ) ;
#39213=CARTESIAN_POINT ( 'NONE',  ( -52.19864025407932928, -11.16676068567596047, 1.871793189971100668 ) ) ;
#39220=ORIENTED_EDGE ( 'NONE', *, *, #49042, .T. ) ;
#39223=LINE ( 'NONE', #5417, #54358 ) ;
#39236=CARTESIAN_POINT ( 'NONE',  ( -71.75000000000000000, -0.9999999999999995559, 20.00000000000000000 ) ) ;
#39249=LINE ( 'NONE', #65948, #63093 ) ;
#39257=CARTESIAN_POINT ( 'NONE',  ( -57.11974195712093660, -8.499999999999992895, 0.06931351858119066955 ) ) ;
#39271=CARTESIAN_POINT ( 'NONE',  ( -55.34553025815903027, -8.494271767728079681, -2.227830982676734628 ) ) ;
#39303=CARTESIAN_POINT ( 'NONE',  ( -30.38025804287907405, -8.500000000000000000, 7.999999999999986677 ) ) ;
#39378=LINE ( 'NONE', #6292, #47937 ) ;
#39442=EDGE_LOOP ( 'NONE', ( #40219, #31918, #8377, #60002 ) ) ;
#39467=EDGE_LOOP ( 'NONE', ( #64464, #67133 ) ) ;
#39514=EDGE_LOOP ( 'NONE', ( #27567, #25909, #34090 ) ) ;
#39519=AXIS2_PLACEMENT_3D ( 'NONE', #59213, #31105, #42768 ) ;
#39521=EDGE_CURVE ( 'NONE', #21141, #23645, #21779, .T. ) ;
#39529=ORIENTED_EDGE ( 'NONE', *, *, #22813, .F. ) ;
#39564=CARTESIAN_POINT ( 'NONE',  ( -50.50422316360081965, -10.70702235289599002, 3.851429980451545276 ) ) ;
#39647=CARTESIAN_POINT ( 'NONE',  ( -75.50000000000000000, -6.499999999999992006, 21.00000000000000000 ) ) ;
#39766=CARTESIAN_POINT ( 'NONE',  ( -29.91370621994125756, -7.761720733523188365, -0.7755720678490063413 ) ) ;
#39801=VERTEX_POINT ( 'NONE', #33700 ) ;
#39812=VECTOR ( 'NONE', #56389, 1000.000000000000000 ) ;
#39832=CARTESIAN_POINT ( 'NONE',  ( -49.16900266361303551, -11.26963036414519337, 3.521240599371135094 ) ) ;
#39849=EDGE_LOOP ( 'NONE', ( #32650, #1222, #1558, #6685 ) ) ;
#39850=ADVANCED_FACE ( 'NONE', ( #50245 ), #37841, .F. ) ;
#39875=AXIS2_PLACEMENT_3D ( 'NONE', #49724, #21229, #43104 ) ;
#39878=CARTESIAN_POINT ( 'NONE',  ( -87.50000000000000000, -6.499999999999990230, 3.000000000000000000 ) ) ;
#39906=ORIENTED_EDGE ( 'NONE', *, *, #27155, .T. ) ;
#39914=DIRECTION ( 'NONE',  ( -0.6163733505331072671, 0.000000000000000000, -0.7874540575504017648 ) ) ;
#39924=EDGE_LOOP ( 'NONE', ( #23592, #3135, #2887 ) ) ;
#39934=CARTESIAN_POINT ( 'NONE',  ( -28.74999999999999645, -8.499999999999996447, 15.00000000000000178 ) ) ;
#39980=ORIENTED_EDGE ( 'NONE', *, *, #49336, .T. ) ;
#39995=AXIS2_PLACEMENT_3D ( 'NONE', #49354, #34210, #28194 ) ;
#40034=CARTESIAN_POINT ( 'NONE',  ( -33.89861118948982721, -9.947368421052628307, 2.722470280083841843 ) ) ;
#40065=EDGE_LOOP ( 'NONE', ( #24618, #27626, #32334, #545 ) ) ;
#40071=( BOUNDED_SURFACE ( )  B_SPLINE_SURFACE ( 3, 2, ( 
 ( #28626, #22680, #1849 ),
 ( #44183, #17431, #38899 ),
 ( #60302, #12106, #55006 ),
 ( #6834, #23032, #44529 ) ),
 .UNSPECIFIED., .F., .F., .F. ) 
 B_SPLINE_SURFACE_WITH_KNOTS ( ( 4, 4 ),
 ( 3, 3 ),
 ( 8.673617379884035472E-19, 0.002371732043478174713 ),
 ( 0.000000000000000000, 1.000000000000000000 ),
 .UNSPECIFIED. ) 
 GEOMETRIC_REPRESENTATION_ITEM ( )  RATIONAL_B_SPLINE_SURFACE ( (
 ( 1.000000000000000000, 0.9473232638932230776, 1.000000000000000000),
 ( 1.000000000000000000, 0.9785952379394217138, 1.000000000000000000),
 ( 1.000000000000000000, 1.000279878396956645, 1.000000000000000000),
 ( 1.000000000000000000, 1.000000000000000000, 1.000000000000000000) ) ) 
 REPRESENTATION_ITEM ( '' )  SURFACE ( )  );
#40095=CARTESIAN_POINT ( 'NONE',  ( -30.87808905615140276, -8.491754569869277347, -1.062615821289257356 ) ) ;
#40107=ORIENTED_EDGE ( 'NONE', *, *, #14463, .F. ) ;
#40112=CARTESIAN_POINT ( 'NONE',  ( -57.11974195712093660, -8.499999999999992895, 0.06931351858119066955 ) ) ;
#40121=DIRECTION ( 'NONE',  ( 1.000000000000000000, -1.445602896647339656E-16, 0.000000000000000000 ) ) ;
#40145=CARTESIAN_POINT ( 'NONE',  ( -16.75000000000000000, -3.000000000000000000, 24.00000000000000000 ) ) ;
#40219=ORIENTED_EDGE ( 'NONE', *, *, #25746, .T. ) ;
#40242=CARTESIAN_POINT ( 'NONE',  ( -51.84221223720477667, -9.947368421052628307, 4.481646853389227303 ) ) ;
#40256=FACE_OUTER_BOUND ( 'NONE', #37605, .T. ) ;
#40288=FILL_AREA_STYLE ('',( #57488 ) ) ;
#40291=ORIENTED_EDGE ( 'NONE', *, *, #57249, .F. ) ;
#40317=VERTEX_POINT ( 'NONE', #3298 ) ;
#40324=VERTEX_POINT ( 'NONE', #8639 ) ;
#40402=CARTESIAN_POINT ( 'NONE',  ( -54.39629169766776329, -9.126466545921049445, -3.681448577167658609 ) ) ;
#40455=FACE_OUTER_BOUND ( 'NONE', #48272, .T. ) ;
#40510=CARTESIAN_POINT ( 'NONE',  ( -32.15258571259099085, -8.506466480591909018, -2.217585092922450318 ) ) ;
#40511=DIRECTION ( 'NONE',  ( -1.000000000000000000, -0.000000000000000000, 0.000000000000000000 ) ) ;
#40518=CARTESIAN_POINT ( 'NONE',  ( -56.14388227616464633, -8.500000000000000000, 7.349426879366860454 ) ) ;
#40524=CARTESIAN_POINT ( 'NONE',  ( -42.80240508717511005, -12.17312045095308903, 3.179269702374134976 ) ) ;
#40556=ORIENTED_EDGE ( 'NONE', *, *, #27948, .F. ) ;
#40563=FACE_OUTER_BOUND ( 'NONE', #44910, .T. ) ;
#40601=ORIENTED_EDGE ( 'NONE', *, *, #3863, .T. ) ;
#40621=AXIS2_PLACEMENT_3D ( 'NONE', #318, #64051, #11975 ) ;
#40643=CARTESIAN_POINT ( 'NONE',  ( -3.000000000000000000, -2.499999999999999556, 24.00000000000000000 ) ) ;
#40692=CARTESIAN_POINT ( 'NONE',  ( -70.75000000000000000, -4.000000000000000000, 20.00000000000000000 ) ) ;
#40695=AXIS2_PLACEMENT_3D ( 'NONE', #49706, #22973, #39173 ) ;
#40723=DIRECTION ( 'NONE',  ( -0.000000000000000000, -1.000000000000000000, -0.000000000000000000 ) ) ;
#40726=DIRECTION ( 'NONE',  ( 1.000000000000000000, -1.189524669241239115E-16, -0.000000000000000000 ) ) ;
#40731=CARTESIAN_POINT ( 'NONE',  ( -75.75000000000000000, -3.000000000000000000, 19.00000000000000000 ) ) ;
#40819=CARTESIAN_POINT ( 'NONE',  ( -75.75000000000000000, -3.000000000000000000, 7.000000000000001776 ) ) ;
#40821=CARTESIAN_POINT ( 'NONE',  ( -75.50000000000000000, -6.499999999999992006, 3.000000000000000000 ) ) ;
#40889=DIRECTION ( 'NONE',  ( 0.5792071321891958391, 0.5736185108958186118, 0.5792071321891946178 ) ) ;
#40914=AXIS2_PLACEMENT_3D ( 'NONE', #41754, #67402, #14646 ) ;
#40992=AXIS2_PLACEMENT_3D ( 'NONE', #64184, #59236, #58568 ) ;
#41000=LINE ( 'NONE', #35697, #9044 ) ;
#41050=CYLINDRICAL_SURFACE ( 'NONE', #11864, 4.999999999999997335 ) ;
#41095=VERTEX_POINT ( 'NONE', #23498 ) ;
#41115=CARTESIAN_POINT ( 'NONE',  ( -12.74999999999999822, -4.000000000000000000, 18.00000000000000000 ) ) ;
#41122=VECTOR ( 'NONE', #62764, 1000.000000000000000 ) ;
#41161=DIRECTION ( 'NONE',  ( -0.7239014318314619389, -0.3935725838164222390, -0.5666280422467853128 ) ) ;
#41175=DIRECTION ( 'NONE',  ( -1.000000000000000000, -1.084202172485503448E-16, 0.000000000000000000 ) ) ;
#41206=DIRECTION ( 'NONE',  ( 0.000000000000000000, 0.000000000000000000, 1.000000000000000000 ) ) ;
#41220=CARTESIAN_POINT ( 'NONE',  ( -52.56905535911819527, -9.512283121613261727, 4.966208934664647856 ) ) ;
#41251=ADVANCED_FACE ( 'NONE', ( #55866 ), #25635, .F. ) ;
#41252=ADVANCED_FACE ( 'NONE', ( #46396 ), #24196, .F. ) ;
#41308=DIRECTION ( 'NONE',  ( -1.000000000000000000, 0.000000000000000000, 0.000000000000000000 ) ) ;
#41330=EDGE_CURVE ( 'NONE', #681, #26367, #32670, .T. ) ;
#41337=VERTEX_POINT ( 'NONE', #17115 ) ;
#41369=DIRECTION ( 'NONE',  ( -1.000000000000000000, 0.000000000000000000, 0.000000000000000000 ) ) ;
#41420=CARTESIAN_POINT ( 'NONE',  ( -28.74999999999999645, -4.000000000000000000, 15.00000000000000178 ) ) ;
#41423=EDGE_CURVE ( 'NONE', #38572, #48124, #67381, .T. ) ;
#41432=ORIENTED_EDGE ( 'NONE', *, *, #3664, .F. ) ;
#41500=CARTESIAN_POINT ( 'NONE',  ( -87.50000000000000000, -6.499999999999990230, 21.00000000000000000 ) ) ;
#41555=CARTESIAN_POINT ( 'NONE',  ( 0.000000000000000000, -4.000000000000000000, 18.00000000000000000 ) ) ;
#41580=CARTESIAN_POINT ( 'NONE',  ( -7.731910350068054619E-16, -6.500000000000000888, 21.00000000000000000 ) ) ;
#41610=ORIENTED_EDGE ( 'NONE', *, *, #42237, .T. ) ;
#41693=DIRECTION ( 'NONE',  ( 1.000000000000000000, 0.000000000000000000, 0.000000000000000000 ) ) ;
#41754=CARTESIAN_POINT ( 'NONE',  ( -3.000000000000000000, -2.499999999999999556, 24.00000000000000000 ) ) ;
#41759=ORIENTED_EDGE ( 'NONE', *, *, #30734, .T. ) ;
#41781=CARTESIAN_POINT ( 'NONE',  ( -74.75000000000000000, 4.336808689942017736E-16, 7.000000000000001776 ) ) ;
#41795=CARTESIAN_POINT ( 'NONE',  ( -12.74999999999999822, -3.000000000000000000, 7.000000000000001776 ) ) ;
#41806=ORIENTED_EDGE ( 'NONE', *, *, #26897, .T. ) ;
#41832=AXIS2_PLACEMENT_3D ( 'NONE', #37146, #31459, #41369 ) ;
#41838=ORIENTED_EDGE ( 'NONE', *, *, #67053, .T. ) ;
#41855=DIRECTION ( 'NONE',  ( -0.000000000000000000, 1.000000000000000000, -0.000000000000000000 ) ) ;
#41861=ORIENTED_EDGE ( 'NONE', *, *, #43064, .T. ) ;
#41892=ORIENTED_EDGE ( 'NONE', *, *, #12469, .F. ) ;
#41951=UNCERTAINTY_MEASURE_WITH_UNIT (LENGTH_MEASURE( 1.000000000000000082E-05 ), #48360, 'distance_accuracy_value', 'NONE');
#41965=DIRECTION ( 'NONE',  ( 1.000000000000000000, 0.000000000000000000, 0.000000000000000000 ) ) ;
#42007=VERTEX_POINT ( 'NONE', #17999 ) ;
#42041=AXIS2_PLACEMENT_3D ( 'NONE', #24552, #68897, #30177 ) ;
#42043=AXIS2_PLACEMENT_3D ( 'NONE', #497, #139, #32552 ) ;
#42066=LINE ( 'NONE', #58889, #44923 ) ;
#42079=CIRCLE ( 'NONE', #11692, 3.100000000000005418 ) ;
#42085=CARTESIAN_POINT ( 'NONE',  ( 0.000000000000000000, -3.500000000000000000, 0.000000000000000000 ) ) ;
#42087=CARTESIAN_POINT ( 'NONE',  ( -60.16140840056181105, -7.539700457364309827, -0.01736709955687108439 ) ) ;
#42143=EDGE_CURVE ( 'NONE', #3382, #52764, #47104, .T. ) ;
#42149=CARTESIAN_POINT ( 'NONE',  ( -75.75000000000000000, -3.585786437626905077, 19.00000000000000000 ) ) ;
#42197=CARTESIAN_POINT ( 'NONE',  ( -40.70406133565712992, -11.89285714285713880, 3.265330863013266693 ) ) ;
#42202=FACE_OUTER_BOUND ( 'NONE', #18660, .T. ) ;
#42225=FACE_OUTER_BOUND ( 'NONE', #18372, .T. ) ;
#42227=DIRECTION ( 'NONE',  ( 0.000000000000000000, 0.000000000000000000, -1.000000000000000000 ) ) ;
#42237=EDGE_CURVE ( 'NONE', #11986, #5856, #55216, .T. ) ;
#42263=VERTEX_POINT ( 'NONE', #58311 ) ;
#42317=CARTESIAN_POINT ( 'NONE',  ( -75.75000000000000000, -3.000000000000000000, 6.000000000000001776 ) ) ;
#42360=DIRECTION ( 'NONE',  ( -0.000000000000000000, 1.000000000000000000, 0.000000000000000000 ) ) ;
#42376=CARTESIAN_POINT ( 'NONE',  ( -12.74999999999999822, -3.000000000000000000, 0.000000000000000000 ) ) ;
#42418=CARTESIAN_POINT ( 'NONE',  ( -30.83671138439772719, -8.500000000000087041, -0.2331546148446474176 ) ) ;
#42420=LINE ( 'NONE', #48044, #55552 ) ;
#42425=CARTESIAN_POINT ( 'NONE',  ( -60.70461754965443646, -7.499999999999992006, 0.000000000000000000 ) ) ;
#42442=CYLINDRICAL_SURFACE ( 'NONE', #12777, 1.000000000000000888 ) ;
#42472=ADVANCED_FACE ( 'NONE', ( #18842 ), #29768, .T. ) ;
#42479=PLANE ( 'NONE',  #48794 ) ;
#42508=ORIENTED_EDGE ( 'NONE', *, *, #6344, .F. ) ;
#42563=ORIENTED_EDGE ( 'NONE', *, *, #15906, .F. ) ;
#42564=FACE_BOUND ( 'NONE', #47951, .T. ) ;
#42567=CIRCLE ( 'NONE', #39194, 1.000000000000000888 ) ;
#42576=CARTESIAN_POINT ( 'NONE',  ( -87.50000000000000000, -6.499999999999990230, 21.00000000000000000 ) ) ;
#42640=CARTESIAN_POINT ( 'NONE',  ( -32.76851741822840580, -9.107254030101904263, -2.000000000000000000 ) ) ;
#42649=( BOUNDED_CURVE ( )  B_SPLINE_CURVE ( 3, ( #14256, #63137, #52607, #68778 ),
 .UNSPECIFIED., .F., .F. ) 
 B_SPLINE_CURVE_WITH_KNOTS ( ( 4, 4 ),
 ( 1.570796326794896780, 2.351346768814402743 ),
 .UNSPECIFIED. ) 
 CURVE ( )  GEOMETRIC_REPRESENTATION_ITEM ( )  RATIONAL_B_SPLINE_CURVE ( ( 1.000000000000000000, 0.9498695926598449413, 0.9498695926598449413, 1.000000000000000000 ) ) 
 REPRESENTATION_ITEM ( '' )  );
#42684=B_SPLINE_CURVE_WITH_KNOTS ( 'NONE', 3,
 ( #39257, #810, #22018, #55399, #27253, #48785, #64584, #6861, #65954, #33936 ),
 .UNSPECIFIED., .F., .F.,
 ( 4, 2, 2, 2, 4 ),
 ( 6.776263578034402713E-20, 0.0008170663553932240456, 0.001634132710786447874, 0.002451199066179671811, 0.003268265421572895749 ),
 .UNSPECIFIED. ) ;
#42745=DIRECTION ( 'NONE',  ( -1.189524669241239115E-16, -1.000000000000000000, -0.000000000000000000 ) ) ;
#42762=CARTESIAN_POINT ( 'NONE',  ( -31.24938216804229185, -8.559564029643235372, -0.5720419862225104568 ) ) ;
#42768=DIRECTION ( 'NONE',  ( -1.000000000000000000, 0.000000000000000000, 0.000000000000000000 ) ) ;
#42818=DIRECTION ( 'NONE',  ( 0.000000000000000000, 1.000000000000000000, 0.000000000000000000 ) ) ;
#42826=VECTOR ( 'NONE', #18563, 1000.000000000000000 ) ;
#42840=AXIS2_PLACEMENT_3D ( 'NONE', #59977, #7217, #49786 ) ;
#42855=EDGE_LOOP ( 'NONE', ( #52116, #8017, #33446, #21226, #294 ) ) ;
#42870=ORIENTED_EDGE ( 'NONE', *, *, #17548, .F. ) ;
#42878=ADVANCED_FACE ( 'NONE', ( #40256 ), #40071, .T. ) ;
#42932=LINE ( 'NONE', #5563, #65739 ) ;
#42965=DIRECTION ( 'NONE',  ( -1.189524669241239115E-16, -1.000000000000000000, 0.000000000000000000 ) ) ;
#43001=CARTESIAN_POINT ( 'NONE',  ( -87.50000000000000000, -3.500000000000000000, 24.00000000000000000 ) ) ;
#43008=ADVANCED_FACE ( 'NONE', ( #46247 ), #30346, .T. ) ;
#43009=EDGE_CURVE ( 'NONE', #26367, #57528, #30562, .T. ) ;
#43019=EDGE_CURVE ( 'NONE', #24199, #25898, #49027, .T. ) ;
#43025=CARTESIAN_POINT ( 'NONE',  ( -57.48951619522433276, -8.499999999999994671, -0.6003161102123086845 ) ) ;
#43029=VERTEX_POINT ( 'NONE', #15614 ) ;
#43064=EDGE_CURVE ( 'NONE', #32747, #1828, #66197, .T. ) ;
#43069=CARTESIAN_POINT ( 'NONE',  ( -54.54999176738918010, -9.007918291183415249, 4.145374715402367016 ) ) ;
#43081=CARTESIAN_POINT ( 'NONE',  ( -33.69829734337137239, -9.571662231021266010, -3.215428675379258916 ) ) ;
#43082=LINE ( 'NONE', #64130, #24645 ) ;
#43084=( NAMED_UNIT ( * ) SI_UNIT ( $, .STERADIAN. ) SOLID_ANGLE_UNIT ( ) );
#43094=ADVANCED_FACE ( 'NONE', ( #64811 ), #26478, .F. ) ;
#43095=DIRECTION ( 'NONE',  ( 0.000000000000000000, 0.000000000000000000, 1.000000000000000000 ) ) ;
#43102=DIRECTION ( 'NONE',  ( 0.000000000000000000, 0.000000000000000000, -1.000000000000000000 ) ) ;
#43104=DIRECTION ( 'NONE',  ( -1.000000000000000000, 1.084202172485504434E-16, 0.000000000000000000 ) ) ;
#43110=CARTESIAN_POINT ( 'NONE',  ( -53.60138881051016568, -9.947368421052624754, -7.000000000000000000 ) ) ;
#43121=DIRECTION ( 'NONE',  ( 0.000000000000000000, 0.000000000000000000, 1.000000000000000000 ) ) ;
#43200=CARTESIAN_POINT ( 'NONE',  ( -11.74999999999999645, -4.000000000000000000, 19.00000000000000000 ) ) ;
#43294=ORIENTED_EDGE ( 'NONE', *, *, #15996, .T. ) ;
#43308=DIRECTION ( 'NONE',  ( -0.8753987966738354665, 3.570037141435574061E-13, -0.4834014344020927112 ) ) ;
#43312=DIRECTION ( 'NONE',  ( 1.000000000000000000, 0.000000000000000000, 0.000000000000000000 ) ) ;
#43349=DIRECTION ( 'NONE',  ( 1.000000000000000000, 0.000000000000000000, 0.000000000000000000 ) ) ;
#43358=ORIENTED_EDGE ( 'NONE', *, *, #19029, .T. ) ;
#43407=EDGE_CURVE ( 'NONE', #24199, #29573, #27067, .T. ) ;
#43417=VERTEX_POINT ( 'NONE', #1337 ) ;
#43423=DIRECTION ( 'NONE',  ( -1.000000000000000000, 0.000000000000000000, 0.000000000000000000 ) ) ;
#43435=CARTESIAN_POINT ( 'NONE',  ( -74.75000000000000000, -0.9999999999999995559, 5.000000000000001776 ) ) ;
#43445=CARTESIAN_POINT ( 'NONE',  ( -42.59563188260839439, -13.96749343005688715, 0.7786704236754057318 ) ) ;
#43497=EDGE_CURVE ( 'NONE', #41337, #17478, #44015, .T. ) ;
#43564=DIRECTION ( 'NONE',  ( 0.000000000000000000, -1.000000000000000000, -0.000000000000000000 ) ) ;
#43618=LINE ( 'NONE', #66407, #64717 ) ;
#43628=CARTESIAN_POINT ( 'NONE',  ( -54.10983016445163685, -9.443832887532138898, -2.000000000000000000 ) ) ;
#43638=CARTESIAN_POINT ( 'NONE',  ( 0.000000000000000000, -4.000000000000000000, 7.000000000000001776 ) ) ;
#43662=LINE ( 'NONE', #38735, #64309 ) ;
#43713=CARTESIAN_POINT ( 'NONE',  ( -51.84221223720477667, -9.947368421052628307, 4.481646853389226415 ) ) ;
#43719=EDGE_CURVE ( 'NONE', #5856, #18813, #4834, .T. ) ;
#43723=CARTESIAN_POINT ( 'NONE',  ( -33.42999993322085572, -9.448433432980072766, -2.594157102514449420 ) ) ;
#43725=ORIENTED_EDGE ( 'NONE', *, *, #35689, .T. ) ;
#43732=VECTOR ( 'NONE', #34878, 1000.000000000000000 ) ;
#43746=CARTESIAN_POINT ( 'NONE',  ( -75.75000000000000000, -4.000000000000000000, 19.00000000000000000 ) ) ;
#43767=EDGE_LOOP ( 'NONE', ( #23877, #27769, #60783, #65565 ) ) ;
#43772=VECTOR ( 'NONE', #21953, 1000.000000000000000 ) ;
#43813=VECTOR ( 'NONE', #8941, 1000.000000000000000 ) ;
#43886=EDGE_LOOP ( 'NONE', ( #27298, #69184, #35651, #34764 ) ) ;
#43980=DIRECTION ( 'NONE',  ( 0.000000000000000000, 0.000000000000000000, 1.000000000000000000 ) ) ;
#43983=ORIENTED_EDGE ( 'NONE', *, *, #7449, .F. ) ;
#44015=LINE ( 'NONE', #6656, #51656 ) ;
#44107=VECTOR ( 'NONE', #45543, 1000.000000000000000 ) ;
#44120=EDGE_CURVE ( 'NONE', #3393, #45684, #4413, .T. ) ;
#44121=CARTESIAN_POINT ( 'NONE',  ( -43.26576733027980026, -14.00568869182241016, 2.673603619738250892 ) ) ;
#44122=ORIENTED_EDGE ( 'NONE', *, *, #462, .F. ) ;
#44183=CARTESIAN_POINT ( 'NONE',  ( -54.37283216165869248, -9.131344072907124243, -2.873593582808337210 ) ) ;
#44203=DIRECTION ( 'NONE',  ( -1.000000000000000000, 0.000000000000000000, 0.000000000000000000 ) ) ;
#44206=PRODUCT_CONTEXT ( 'NONE', #32097, 'mechanical' ) ;
#44225=EDGE_CURVE ( 'NONE', #17714, #63631, #23632, .T. ) ;
#44226=CIRCLE ( 'NONE', #26340, 1.000000000000000888 ) ;
#44230=DIRECTION ( 'NONE',  ( 1.000000000000000000, 0.000000000000000000, -0.000000000000000000 ) ) ;
#44281=CARTESIAN_POINT ( 'NONE',  ( -35.65778776279521622, -9.947368421052628307, 4.481646853389228191 ) ) ;
#44296=EDGE_CURVE ( 'NONE', #45684, #26721, #17695, .T. ) ;
#44341=CARTESIAN_POINT ( 'NONE',  ( -75.75000000000000000, -4.000000000000000000, 6.000000000000001776 ) ) ;
#44351=ORIENTED_EDGE ( 'NONE', *, *, #807, .F. ) ;
#44376=EDGE_CURVE ( 'NONE', #63964, #39801, #9909, .T. ) ;
#44435=CARTESIAN_POINT ( 'NONE',  ( -34.17996781353688363, -10.00128081186360696, -3.271960291194134562 ) ) ;
#44440=ORIENTED_EDGE ( 'NONE', *, *, #28000, .F. ) ;
#44456=DIRECTION ( 'NONE',  ( 1.000000000000000000, 0.000000000000000000, -0.000000000000000000 ) ) ;
#44484=ORIENTED_EDGE ( 'NONE', *, *, #43719, .T. ) ;
#44499=LINE ( 'NONE', #18064, #65545 ) ;
#44501=AXIS2_PLACEMENT_3D ( 'NONE', #64237, #57590, #151 ) ;
#44529=CARTESIAN_POINT ( 'NONE',  ( -53.18756747357344494, -10.02680648607920588, -3.499999999999314770 ) ) ;
#44536=DIRECTION ( 'NONE',  ( 0.000000000000000000, 0.000000000000000000, -1.000000000000000000 ) ) ;
#44539=EDGE_CURVE ( 'NONE', #48229, #24594, #56152, .T. ) ;
#44543=DIRECTION ( 'NONE',  ( 0.000000000000000000, 0.000000000000000000, 1.000000000000000000 ) ) ;
#44604=EDGE_CURVE ( 'NONE', #62964, #31013, #61706, .T. ) ;
#44610=DIRECTION ( 'NONE',  ( 1.000000000000000000, 0.000000000000000000, 0.000000000000000000 ) ) ;
#44626=CARTESIAN_POINT ( 'NONE',  ( -39.06014859142244688, -13.20604375391146945, 2.745267173635231650 ) ) ;
#44631=DIRECTION ( 'NONE',  ( 0.5792071321891931746, -0.5736185108958206103, -0.5792071321891952840 ) ) ;
#44660=DIRECTION ( 'NONE',  ( 1.000000000000000000, 0.000000000000000000, 0.000000000000000000 ) ) ;
#44665=FACE_OUTER_BOUND ( 'NONE', #77, .T. ) ;
#44666=LINE ( 'NONE', #66059, #11481 ) ;
#44683=CARTESIAN_POINT ( 'NONE',  ( -76.75000000000000000, 4.336808689942018722E-16, 6.000000000000001776 ) ) ;
#44730=CARTESIAN_POINT ( 'NONE',  ( -47.71347897792735182, -13.42724224818812218, 0.9185643661976420349 ) ) ;
#44761=ADVANCED_FACE ( 'NONE', ( #18639 ), #45414, .T. ) ;
#44774=ORIENTED_EDGE ( 'NONE', *, *, #12860, .T. ) ;
#44795=ADVANCED_FACE ( 'NONE', ( #63276 ), #46086, .T. ) ;
#44846=CARTESIAN_POINT ( 'NONE',  ( -53.01121866695765306, -10.53184416402257284, 3.891476709836705794 ) ) ;
#44900=CARTESIAN_POINT ( 'NONE',  ( -56.63152288741350304, -7.947250274547568161, -1.331476843523650588 ) ) ;
#44910=EDGE_LOOP ( 'NONE', ( #10703, #60725, #53786, #18578 ) ) ;
#44923=VECTOR ( 'NONE', #48718, 1000.000000000000000 ) ;
#44960=CARTESIAN_POINT ( 'NONE',  ( -36.08832455125276084, -11.72126376154535521, 1.574586324192390085 ) ) ;
#44969=CARTESIAN_POINT ( 'NONE',  ( 3.851859888774471706E-31, -8.500000000000000000, 1.000000000000000888 ) ) ;
#44985=ADVANCED_FACE ( 'NONE', ( #20715 ), #5203, .T. ) ;
#44996=ORIENTED_EDGE ( 'NONE', *, *, #53533, .F. ) ;
#44997=ADVANCED_FACE ( 'NONE', ( #26648 ), #55042, .F. ) ;
#45033=CARTESIAN_POINT ( 'NONE',  ( -32.39845779402550363, -8.920930673357418073, -1.643626324569322117 ) ) ;
#45056=LINE ( 'NONE', #55208, #6938 ) ;
#45076=DIRECTION ( 'NONE',  ( 0.000000000000000000, 0.000000000000000000, 1.000000000000000000 ) ) ;
#45120=VERTEX_POINT ( 'NONE', #50408 ) ;
#45131=CIRCLE ( 'NONE', #66412, 1.000000000000000888 ) ;
#45138=DIRECTION ( 'NONE',  ( -0.000000000000000000, -0.000000000000000000, 1.000000000000000000 ) ) ;
#45184=EDGE_CURVE ( 'NONE', #62964, #10674, #14871, .T. ) ;
#45193=CARTESIAN_POINT ( 'NONE',  ( -51.50115812098317036, -11.66198514980602674, 1.604287519264194550 ) ) ;
#45212=DIRECTION ( 'NONE',  ( -1.000000000000000000, 0.000000000000000000, 0.000000000000000000 ) ) ;
#45215=CARTESIAN_POINT ( 'NONE',  ( -74.75000000000000000, -4.000000000000000000, 7.000000000000001776 ) ) ;
#45300=ADVANCED_FACE ( 'NONE', ( #11993 ), #16653, .T. ) ;
#45317=VECTOR ( 'NONE', #40511, 1000.000000000000000 ) ;
#45320=( BOUNDED_SURFACE ( )  B_SPLINE_SURFACE ( 3, 2, ( 
 ( #2001, #55889, #51311 ),
 ( #50278, #18618, #67137 ),
 ( #29127, #40095, #34766 ),
 ( #66442, #14023, #50965 ),
 ( #7690, #713, #56580 ),
 ( #45033, #8745, #35128 ),
 ( #45384, #62199, #8049 ),
 ( #13308, #18259, #35484 ) ),
 .UNSPECIFIED., .F., .F., .F. ) 
 B_SPLINE_SURFACE_WITH_KNOTS ( ( 4, 2, 2, 4 ),
 ( 3, 3 ),
 ( -1.357421119951851551E-16, 0.001805431820033041824, 0.002708147730049630716, 0.003610863640066219390 ),
 ( 0.000000000000000000, 1.000000000000000000 ),
 .UNSPECIFIED. ) 
 GEOMETRIC_REPRESENTATION_ITEM ( )  RATIONAL_B_SPLINE_SURFACE ( (
 ( 1.000000000000000000, 0.7942671885214119820, 1.000000000000000000),
 ( 1.000000000000000000, 0.8220809233579065012, 1.000000000000000000),
 ( 1.000000000000000000, 0.8510448064981840366, 1.000000000000000000),
 ( 1.000000000000000000, 0.8908666667640210424, 1.000000000000000000),
 ( 1.000000000000000000, 0.9035567410623921436, 1.000000000000000000),
 ( 1.000000000000000000, 0.9270715898449251036, 1.000000000000000000),
 ( 1.000000000000000000, 0.9379207207978137451, 1.000000000000000000),
 ( 1.000000000000000000, 0.9473232638932225225, 1.000000000000000000) ) ) 
 REPRESENTATION_ITEM ( '' )  SURFACE ( )  );
#45346=ORIENTED_EDGE ( 'NONE', *, *, #22241, .T. ) ;
#45381=ORIENTED_EDGE ( 'NONE', *, *, #68381, .T. ) ;
#45384=CARTESIAN_POINT ( 'NONE',  ( -32.58435833479455113, -9.007129948131591846, -1.827021129109788644 ) ) ;
#45403=CARTESIAN_POINT ( 'NONE',  ( -60.70461754965443646, -8.499999999999992895, 1.000000000000000000 ) ) ;
#45414=PLANE ( 'NONE',  #65193 ) ;
#45426=ORIENTED_EDGE ( 'NONE', *, *, #50690, .T. ) ;
#45427=DIRECTION ( 'NONE',  ( 0.000000000000000000, 0.000000000000000000, 1.000000000000000000 ) ) ;
#45517=CARTESIAN_POINT ( 'NONE',  ( -71.75000000000000000, -0.9999999999999995559, 19.00000000000000000 ) ) ;
#45537=DIRECTION ( 'NONE',  ( -1.000000000000000000, 0.000000000000000000, 0.000000000000000000 ) ) ;
#45543=DIRECTION ( 'NONE',  ( -0.000000000000000000, 0.000000000000000000, -1.000000000000000000 ) ) ;
#45548=CARTESIAN_POINT ( 'NONE',  ( -51.72259415970177798, -11.52611143915721037, 3.270167026231387997 ) ) ;
#45565=ADVANCED_FACE ( 'NONE', ( #48813 ), #48460, .T. ) ;
#45577=CARTESIAN_POINT ( 'NONE',  ( -36.00278222459130006, -10.17514555344026306, 4.251650545525158975 ) ) ;
#45598=PRESENTATION_STYLE_ASSIGNMENT (( #61695 ) ) ;
#45604=CARTESIAN_POINT ( 'NONE',  ( 3.851859888774471706E-31, -8.500000000000000000, 1.000000000000000888 ) ) ;
#45613=CARTESIAN_POINT ( 'NONE',  ( -16.75000000000000000, -3.000000000000000000, 19.00000000000000000 ) ) ;
#45621=VECTOR ( 'NONE', #53111, 1000.000000000000000 ) ;
#45625=CARTESIAN_POINT ( 'NONE',  ( -32.38286428517920257, -8.500000000000000000, 6.664929171799900409 ) ) ;
#45630=DIRECTION ( 'NONE',  ( 0.000000000000000000, -0.000000000000000000, 1.000000000000000000 ) ) ;
#45642=LINE ( 'NONE', #40692, #7108 ) ;
#45643=ADVANCED_FACE ( 'NONE', ( #55424 ), #12152, .F. ) ;
#45659=CARTESIAN_POINT ( 'NONE',  ( -37.68484432981706789, -12.63346336609729370, 1.177413386875751256 ) ) ;
#45684=VERTEX_POINT ( 'NONE', #56827 ) ;
#45716=ORIENTED_EDGE ( 'NONE', *, *, #52683, .T. ) ;
#45793=CARTESIAN_POINT ( 'NONE',  ( -30.86848549628973615, -7.933252306487679206, -1.326499884503476334 ) ) ;
#45814=CARTESIAN_POINT ( 'NONE',  ( -33.72126112590540004, -9.584527543374615988, -3.208686727472596978 ) ) ;
#45832=VERTEX_POINT ( 'NONE', #42085 ) ;
#45844=DIRECTION ( 'NONE',  ( 1.000000000000000000, -1.189524669241239115E-16, 0.000000000000000000 ) ) ;
#45858=CARTESIAN_POINT ( 'NONE',  ( 0.000000000000000000, -3.500000000000000000, 0.000000000000000000 ) ) ;
#45868=EDGE_CURVE ( 'NONE', #10026, #63373, #68738, .T. ) ;
#45898=ORIENTED_EDGE ( 'NONE', *, *, #7252, .F. ) ;
#45915=CARTESIAN_POINT ( 'NONE',  ( -53.56480923418825313, -9.954352215710184026, -2.522777614992231410 ) ) ;
#45917=SURFACE_STYLE_FILL_AREA ( #40288 ) ;
#45955=CARTESIAN_POINT ( 'NONE',  ( -69.74999999999998579, -4.000000000000000000, 0.000000000000000000 ) ) ;
#45978=AXIS2_PLACEMENT_3D ( 'NONE', #39236, #34603, #66634 ) ;
#46008=VERTEX_POINT ( 'NONE', #25416 ) ;
#46011=CARTESIAN_POINT ( 'NONE',  ( -53.60138881051016568, -9.947368421052624754, -2.000000000000000000 ) ) ;
#46031=LINE ( 'NONE', #24184, #27477 ) ;
#46040=CARTESIAN_POINT ( 'NONE',  ( -54.69521332591794760, -9.106085870126005233, -2.687031549327465907 ) ) ;
#46056=VECTOR ( 'NONE', #45138, 1000.000000000000000 ) ;
#46086=PLANE ( 'NONE',  #35998 ) ;
#46135=DIRECTION ( 'NONE',  ( 0.000000000000000000, 0.000000000000000000, -1.000000000000000000 ) ) ;
#46168=DIRECTION ( 'NONE',  ( -1.000000000000000000, 0.000000000000000000, 0.000000000000000000 ) ) ;
#46171=EDGE_CURVE ( 'NONE', #34584, #51653, #37387, .T. ) ;
#46224=EDGE_LOOP ( 'NONE', ( #27972, #18218, #41806, #37657 ) ) ;
#46233=LINE ( 'NONE', #7849, #39812 ) ;
#46247=FACE_OUTER_BOUND ( 'NONE', #46913, .T. ) ;
#46273=DIRECTION ( 'NONE',  ( -0.000000000000000000, -0.000000000000000000, 1.000000000000000000 ) ) ;
#46316=AXIS2_PLACEMENT_3D ( 'NONE', #61265, #16994, #2101 ) ;
#46322=ORIENTED_EDGE ( 'NONE', *, *, #53258, .F. ) ;
#46323=CARTESIAN_POINT ( 'NONE',  ( -11.74999999999999645, -0.9999999999999995559, 20.00000000000000000 ) ) ;
#46372=FACE_OUTER_BOUND ( 'NONE', #28530, .T. ) ;
#46394=ORIENTED_EDGE ( 'NONE', *, *, #58016, .F. ) ;
#46396=FACE_OUTER_BOUND ( 'NONE', #27151, .T. ) ;
#46397=CARTESIAN_POINT ( 'NONE',  ( -11.74999999999999645, -3.000000000000000000, 19.00000000000000000 ) ) ;
#46432=ORIENTED_EDGE ( 'NONE', *, *, #64319, .T. ) ;
#46474=EDGE_LOOP ( 'NONE', ( #19863, #30263, #43983, #65244 ) ) ;
#46475=CARTESIAN_POINT ( 'NONE',  ( 3.851859888774471706E-31, -8.500000000000000000, 24.00000000000000000 ) ) ;
#46508=CARTESIAN_POINT ( 'NONE',  ( -54.41715584325135069, -9.238994630453190027, 5.297413886133904626 ) ) ;
#46524=DIRECTION ( 'NONE',  ( -1.000000000000000000, 0.000000000000000000, -0.000000000000000000 ) ) ;
#46549=CARTESIAN_POINT ( 'NONE',  ( 3.851859888774471706E-31, -8.500000000000000000, 1.000000000000000888 ) ) ;
#46557=CIRCLE ( 'NONE', #40914, 1.000000000000000000 ) ;
#46561=CARTESIAN_POINT ( 'NONE',  ( -59.62135308701207492, -8.500000000000543565, 0.008598348328329818643 ) ) ;
#46591=LINE ( 'NONE', #67649, #11502 ) ;
#46684=FACE_OUTER_BOUND ( 'NONE', #17665, .T. ) ;
#46689=DIRECTION ( 'NONE',  ( -1.000000000000000000, -0.000000000000000000, 0.000000000000000000 ) ) ;
#46716=CARTESIAN_POINT ( 'NONE',  ( -40.04190075645215785, -13.49999999999999467, 0.8979962945199019275 ) ) ;
#46771=CARTESIAN_POINT ( 'NONE',  ( -33.41658301726149460, -9.461864478049042404, 4.963675025617548364 ) ) ;
#46798=ORIENTED_EDGE ( 'NONE', *, *, #49975, .T. ) ;
#46804=ADVANCED_FACE ( 'NONE', ( #26939 ), #16112, .T. ) ;
#46808=DIRECTION ( 'NONE',  ( -1.000000000000000000, 1.189524669241239115E-16, 0.000000000000000000 ) ) ;
#46810=DIRECTION ( 'NONE',  ( -0.6163733505291654202, 0.000000000000000000, 0.7874540575534871856 ) ) ;
#46812=ADVANCED_FACE ( 'NONE', ( #7516 ), #53699, .F. ) ;
#46893=EDGE_CURVE ( 'NONE', #51117, #56449, #48726, .T. ) ;
#46913=EDGE_LOOP ( 'NONE', ( #68963, #29575, #56865, #55330, #38336, #5394, #4626, #44996, #14066, #60385 ) ) ;
#46928=CARTESIAN_POINT ( 'NONE',  ( -75.50000000000000000, -6.499999999999992006, 21.00000000000000000 ) ) ;
#46946=DIRECTION ( 'NONE',  ( -0.000000000000000000, 1.000000000000000000, 0.000000000000000000 ) ) ;
#46956=ORIENTED_EDGE ( 'NONE', *, *, #47963, .T. ) ;
#46984=FILL_AREA_STYLE ('',( #59193 ) ) ;
#46985=CARTESIAN_POINT ( 'NONE',  ( -17.75000000000000355, -4.000000000000000000, 20.00000000000000000 ) ) ;
#47002=CARTESIAN_POINT ( 'NONE',  ( -34.70658214735873059, -10.70299374098435052, 2.150780036138280060 ) ) ;
#47013=ORIENTED_EDGE ( 'NONE', *, *, #17873, .F. ) ;
#47014=DIRECTION ( 'NONE',  ( -7.703719777548942317E-32, 1.000000000000000000, 0.000000000000000000 ) ) ;
#47079=EDGE_LOOP ( 'NONE', ( #672, #28536, #63427, #8643, #25905, #28409, #34168, #31387, #44122, #11806 ) ) ;
#47094=SURFACE_STYLE_FILL_AREA ( #4459 ) ;
#47096=VECTOR ( 'NONE', #11013, 1000.000000000000000 ) ;
#47104=LINE ( 'NONE', #14722, #12163 ) ;
#47105=EDGE_LOOP ( 'NONE', ( #47013, #16168, #13350, #8728 ) ) ;
#47132=DIRECTION ( 'NONE',  ( -0.000000000000000000, 1.000000000000000000, 0.000000000000000000 ) ) ;
#47135=AXIS2_PLACEMENT_3D ( 'NONE', #59511, #10319, #5349 ) ;
#47195=ORIENTED_EDGE ( 'NONE', *, *, #26508, .T. ) ;
#47199=CARTESIAN_POINT ( 'NONE',  ( -56.46916883648585639, -8.499999999999998224, 7.024140319044985148 ) ) ;
#47201=DIRECTION ( 'NONE',  ( 0.000000000000000000, 0.000000000000000000, 1.000000000000000000 ) ) ;
#47244=ADVANCED_FACE ( 'NONE', ( #20053 ), #48226, .F. ) ;
#47268=LINE ( 'NONE', #46928, #32203 ) ;
#47299=( GEOMETRIC_REPRESENTATION_CONTEXT ( 3 ) GLOBAL_UNCERTAINTY_ASSIGNED_CONTEXT ( ( #58777 ) ) GLOBAL_UNIT_ASSIGNED_CONTEXT ( ( #24762, #7907, #56806 ) ) REPRESENTATION_CONTEXT ( 'NONE', 'WORKASPACE' ) );
#47318=B_SPLINE_CURVE_WITH_KNOTS ( 'NONE', 3,
 ( #47414, #31162, #25543, #61205, #25894, #50317, #57939, #28835 ),
 .UNSPECIFIED., .F., .F.,
 ( 4, 2, 2, 4 ),
 ( 3.510295945092028624E-18, 0.001616916654929161177, 0.002425374982393735043, 0.003233833309858308910 ),
 .UNSPECIFIED. ) ;
#47346=CARTESIAN_POINT ( 'NONE',  ( -38.85043651514852314, -13.12913046416487539, 1.005512611032779891 ) ) ;
#47360=( GEOMETRIC_REPRESENTATION_CONTEXT ( 3 ) GLOBAL_UNCERTAINTY_ASSIGNED_CONTEXT ( ( #67081 ) ) GLOBAL_UNIT_ASSIGNED_CONTEXT ( ( #48697, #53582, #43084 ) ) REPRESENTATION_CONTEXT ( 'NONE', 'WORKASPACE' ) );
#47371=AXIS2_PLACEMENT_3D ( 'NONE', #60006, #7248, #11815 ) ;
#47397=CARTESIAN_POINT ( 'NONE',  ( -39.43665073983763136, -13.33375354601735552, 0.9443502740340453672 ) ) ;
#47401=CARTESIAN_POINT ( 'NONE',  ( 0.000000000000000000, -3.000000000000000000, 18.00000000000000000 ) ) ;
#47413=EDGE_CURVE ( 'NONE', #33018, #20128, #66081, .T. ) ;
#47414=CARTESIAN_POINT ( 'NONE',  ( -26.79538245034556354, -7.499999999999999112, 0.000000000000000000 ) ) ;
#47420=AXIS2_PLACEMENT_3D ( 'NONE', #68923, #30558, #41175 ) ;
#47432=DIRECTION ( 'NONE',  ( 1.000000000000000000, -1.189524669241239115E-16, 0.000000000000000000 ) ) ;
#47507=PLANE ( 'NONE',  #47420 ) ;
#47517=CARTESIAN_POINT ( 'NONE',  ( -75.75000000000000000, -3.000000000000000000, 19.00000000000000000 ) ) ;
#47526=ORIENTED_EDGE ( 'NONE', *, *, #57355, .T. ) ;
#47547=EDGE_CURVE ( 'NONE', #59351, #681, #12912, .T. ) ;
#47562=FACE_OUTER_BOUND ( 'NONE', #64328, .T. ) ;
#47596=ORIENTED_EDGE ( 'NONE', *, *, #51163, .F. ) ;
#47603=CARTESIAN_POINT ( 'NONE',  ( -58.75000000000000000, -4.000000000000000000, 15.00000000000000178 ) ) ;
#47606=DIRECTION ( 'NONE',  ( -0.000000000000000000, -0.000000000000000000, 1.000000000000000000 ) ) ;
#47643=AXIS2_PLACEMENT_3D ( 'NONE', #62371, #30686, #57447 ) ;
#47682=B_SPLINE_CURVE_WITH_KNOTS ( 'NONE', 3,
 ( #57846, #68055, #31080, #37112, #58180, #48022 ),
 .UNSPECIFIED., .F., .F.,
 ( 4, 2, 4 ),
 ( 0.000000000000000000, 0.001170983007612366256, 0.002341966015224732512 ),
 .UNSPECIFIED. ) ;
#47710=DIRECTION ( 'NONE',  ( -0.000000000000000000, -0.000000000000000000, -1.000000000000000000 ) ) ;
#47715=CARTESIAN_POINT ( 'NONE',  ( -33.89861118948982721, -9.947368421052626530, 2.722470280083843619 ) ) ;
#47717=VECTOR ( 'NONE', #12397, 1000.000000000000000 ) ;
#47722=ORIENTED_EDGE ( 'NONE', *, *, #62361, .T. ) ;
#47728=AXIS2_PLACEMENT_3D ( 'NONE', #37852, #69461, #63147 ) ;
#47733=CARTESIAN_POINT ( 'NONE',  ( -10.74999999999999645, 4.336808689942018722E-16, 20.00000000000000000 ) ) ;
#47741=ORIENTED_EDGE ( 'NONE', *, *, #5230, .T. ) ;
#47765=FACE_OUTER_BOUND ( 'NONE', #20867, .T. ) ;
#47776=CARTESIAN_POINT ( 'NONE',  ( -76.75000000000000000, -0.9999999999999995559, 6.000000000000001776 ) ) ;
#47778=FACE_OUTER_BOUND ( 'NONE', #59660, .T. ) ;
#47788=AXIS2_PLACEMENT_3D ( 'NONE', #51756, #47201, #62621 ) ;
#47793=CARTESIAN_POINT ( 'NONE',  ( -40.70406133565712992, -11.89285714285713880, 3.265330863013266693 ) ) ;
#47861=VERTEX_POINT ( 'NONE', #35401 ) ;
#47937=VECTOR ( 'NONE', #17239, 1000.000000000000000 ) ;
#47939=DIRECTION ( 'NONE',  ( -0.000000000000000000, 1.000000000000000000, 0.000000000000000000 ) ) ;
#47948=EDGE_CURVE ( 'NONE', #63631, #3382, #5985, .T. ) ;
#47951=EDGE_LOOP ( 'NONE', ( #24704, #17134 ) ) ;
#47963=EDGE_CURVE ( 'NONE', #20128, #3527, #45642, .T. ) ;
#47971=CARTESIAN_POINT ( 'NONE',  ( -74.75000000000000000, -4.000000000000000000, 18.00000000000000000 ) ) ;
#47983=CARTESIAN_POINT ( 'NONE',  ( -17.75000000000000355, -3.000000000000000000, 0.000000000000000000 ) ) ;
#47987=ORIENTED_EDGE ( 'NONE', *, *, #1452, .T. ) ;
#48003=DIRECTION ( 'NONE',  ( -0.000000000000000000, -0.000000000000000000, 1.000000000000000000 ) ) ;
#48022=CARTESIAN_POINT ( 'NONE',  ( -53.18756747357285519, -10.02680648607945102, -3.500000000000002220 ) ) ;
#48044=CARTESIAN_POINT ( 'NONE',  ( -75.75000000000000000, 4.336808689942018722E-16, 20.00000000000000000 ) ) ;
#48056=ORIENTED_EDGE ( 'NONE', *, *, #651, .F. ) ;
#48062=ORIENTED_EDGE ( 'NONE', *, *, #52683, .F. ) ;
#48076=CYLINDRICAL_SURFACE ( 'NONE', #50324, 3.100000000000003642 ) ;
#48091=ADVANCED_FACE ( 'NONE', ( #42564, #36244, #20730 ), #53758, .T. ) ;
#48110=CARTESIAN_POINT ( 'NONE',  ( -83.49999999999998579, 4.336808689942018722E-16, -5.100000000000000533 ) ) ;
#48124=VERTEX_POINT ( 'NONE', #6959 ) ;
#48126=DIRECTION ( 'NONE',  ( 0.000000000000000000, 1.000000000000000000, -0.000000000000000000 ) ) ;
#48137=CARTESIAN_POINT ( 'NONE',  ( -34.11772421319633253, -9.152876382972609193, 5.508355886455341022 ) ) ;
#48219=EDGE_LOOP ( 'NONE', ( #57632, #10106, #21082, #14055 ) ) ;
#48226=PLANE ( 'NONE',  #63190 ) ;
#48229=VERTEX_POINT ( 'NONE', #46011 ) ;
#48257=ORIENTED_EDGE ( 'NONE', *, *, #58856, .F. ) ;
#48267=CYLINDRICAL_SURFACE ( 'NONE', #25135, 8.499999999999992895 ) ;
#48272=EDGE_LOOP ( 'NONE', ( #61640, #24404 ) ) ;
#48278=AXIS2_PLACEMENT_3D ( 'NONE', #29700, #66283, #44543 ) ;
#48279=TOROIDAL_SURFACE ( 'NONE', #16786, 18.53939201416945082, 5.000000000000000000 ) ;
#48280=CARTESIAN_POINT ( 'NONE',  ( -56.61586366453234831, -8.492381958573840706, -1.066368904513279592 ) ) ;
#48302=FACE_OUTER_BOUND ( 'NONE', #53201, .T. ) ;
#48360=( LENGTH_UNIT ( ) NAMED_UNIT ( * ) SI_UNIT ( .MILLI., .METRE. ) );
#48380=CARTESIAN_POINT ( 'NONE',  ( -34.07680040766327068, -9.981484022772619369, -3.029036331924419123 ) ) ;
#48393=ORIENTED_EDGE ( 'NONE', *, *, #49336, .F. ) ;
#48460=CYLINDRICAL_SURFACE ( 'NONE', #28158, 1.000000000000000000 ) ;
#48496=CYLINDRICAL_SURFACE ( 'NONE', #5303, 1.000000000000000888 ) ;
#48533=DIRECTION ( 'NONE',  ( 0.000000000000000000, -0.000000000000000000, 1.000000000000000000 ) ) ;
#48565=EDGE_CURVE ( 'NONE', #17133, #68588, #25174, .T. ) ;
#48615=DIRECTION ( 'NONE',  ( 1.000000000000000000, 0.000000000000000000, 0.000000000000000000 ) ) ;
#48655=VECTOR ( 'NONE', #22865, 1000.000000000000000 ) ;
#48660=DIRECTION ( 'NONE',  ( -1.000000000000000000, 0.000000000000000000, 0.000000000000000000 ) ) ;
#48662=CARTESIAN_POINT ( 'NONE',  ( -32.76090297675384022, -9.103123100735301065, -2.346905346906288603 ) ) ;
#48691=DIRECTION ( 'NONE',  ( 0.000000000000000000, 0.000000000000000000, 1.000000000000000000 ) ) ;
#48694=CARTESIAN_POINT ( 'NONE',  ( -34.31243252642629926, -10.02680648607947589, -3.499999999999429789 ) ) ;
#48697=( LENGTH_UNIT ( ) NAMED_UNIT ( * ) SI_UNIT ( .MILLI., .METRE. ) );
#48702=CARTESIAN_POINT ( 'NONE',  ( -42.64069574594451950, -13.97002997391379608, 2.674443234125082558 ) ) ;
#48718=DIRECTION ( 'NONE',  ( -0.000000000000000000, -1.000000000000000000, 0.000000000000000000 ) ) ;
#48726=CIRCLE ( 'NONE', #47643, 5.000000000000000000 ) ;
#48732=ADVANCED_FACE ( 'NONE', ( #11731 ), #1098, .T. ) ;
#48748=LINE ( 'NONE', #12788, #69239 ) ;
#48775=VERTEX_POINT ( 'NONE', #22992 ) ;
#48785=CARTESIAN_POINT ( 'NONE',  ( -55.65942242047054123, -8.713741708682274378, -1.106834464302784982 ) ) ;
#48794=AXIS2_PLACEMENT_3D ( 'NONE', #27863, #63874, #28208 ) ;
#48795=CYLINDRICAL_SURFACE ( 'NONE', #18126, 1.000000000000000888 ) ;
#48810=DIRECTION ( 'NONE',  ( 0.000000000000000000, 0.000000000000000000, 1.000000000000000000 ) ) ;
#48813=FACE_OUTER_BOUND ( 'NONE', #23925, .T. ) ;
#48921=VECTOR ( 'NONE', #15733, 1000.000000000000000 ) ;
#48922=CARTESIAN_POINT ( 'NONE',  ( -58.75000000000000000, -4.000000000000000000, 15.00000000000000178 ) ) ;
#48976=DIRECTION ( 'NONE',  ( -0.000000000000000000, -0.000000000000000000, 1.000000000000000000 ) ) ;
#49017=CARTESIAN_POINT ( 'NONE',  ( -40.70406133565712992, -11.08928571428570997, 0.8979962945199000401 ) ) ;
#49027=LINE ( 'NONE', #43746, #11174 ) ;
#49042=EDGE_CURVE ( 'NONE', #2488, #4575, #42932, .T. ) ;
#49045=CARTESIAN_POINT ( 'NONE',  ( -44.93692584854336758, -12.13384599889156945, 3.189947921310896994 ) ) ;
#49049=ORIENTED_EDGE ( 'NONE', *, *, #46171, .F. ) ;
#49158=DIRECTION ( 'NONE',  ( 0.000000000000000000, 0.000000000000000000, 1.000000000000000000 ) ) ;
#49190=ORIENTED_EDGE ( 'NONE', *, *, #42143, .T. ) ;
#49226=ORIENTED_EDGE ( 'NONE', *, *, #8840, .F. ) ;
#49231=PLANE ( 'NONE',  #31808 ) ;
#49238=CARTESIAN_POINT ( 'NONE',  ( -70.75000000000000000, -3.000000000000000000, 19.00000000000000000 ) ) ;
#49250=EDGE_CURVE ( 'NONE', #56578, #2488, #30841, .T. ) ;
#49254=EDGE_CURVE ( 'NONE', #19782, #737, #28717, .T. ) ;
#49317=CARTESIAN_POINT ( 'NONE',  ( -33.85304738437685046, -9.497883372643979527, -3.722847864133452145 ) ) ;
#49336=EDGE_CURVE ( 'NONE', #32528, #4254, #64647, .T. ) ;
#49354=CARTESIAN_POINT ( 'NONE',  ( -43.75000000000000000, 0.000000000000000000, 16.97056274847714974 ) ) ;
#49366=CIRCLE ( 'NONE', #58340, 1.000000000000000888 ) ;
#49434=ADVANCED_FACE ( 'NONE', ( #12497 ), #33961, .F. ) ;
#49493=VERTEX_POINT ( 'NONE', #55775 ) ;
#49507=EDGE_CURVE ( 'NONE', #54282, #10026, #24109, .T. ) ;
#49524=CARTESIAN_POINT ( 'NONE',  ( -35.83032615006315780, -11.56233257873206810, 3.252572872672070847 ) ) ;
#49543=VECTOR ( 'NONE', #58805, 1000.000000000000000 ) ;
#49548=CIRCLE ( 'NONE', #9136, 0.9999999999999987788 ) ;
#49579=LINE ( 'NONE', #43638, #69361 ) ;
#49583=DIRECTION ( 'NONE',  ( -0.000000000000000000, 0.000000000000000000, -1.000000000000000000 ) ) ;
#49585=ORIENTED_EDGE ( 'NONE', *, *, #23428, .F. ) ;
#49627=ORIENTED_EDGE ( 'NONE', *, *, #48565, .T. ) ;
#49651=ORIENTED_EDGE ( 'NONE', *, *, #49507, .T. ) ;
#49656=EDGE_CURVE ( 'NONE', #19259, #45832, #31104, .T. ) ;
#49664=CARTESIAN_POINT ( 'NONE',  ( -33.39017047773998570, -9.443833522994566465, -2.300020890958864861 ) ) ;
#49702=CARTESIAN_POINT ( 'NONE',  ( -75.75000000000000000, -0.9999999999999995559, 6.000000000000001776 ) ) ;
#49706=CARTESIAN_POINT ( 'NONE',  ( -12.74999999999999822, -3.000000000000000000, 7.000000000000001776 ) ) ;
#49723=EDGE_CURVE ( 'NONE', #32327, #59351, #65614, .T. ) ;
#49724=CARTESIAN_POINT ( 'NONE',  ( 0.000000000000000000, -3.500000000000000000, 24.00000000000000000 ) ) ;
#49772=AXIS2_PLACEMENT_3D ( 'NONE', #16462, #16108, #68868 ) ;
#49786=DIRECTION ( 'NONE',  ( 1.000000000000000000, 0.000000000000000000, 0.000000000000000000 ) ) ;
#49794=CARTESIAN_POINT ( 'NONE',  ( -48.85491959229422321, -13.04958088359142288, 1.031244760999817212 ) ) ;
#49851=DIRECTION ( 'NONE',  ( -1.000000000000000000, 0.000000000000000000, 0.000000000000000000 ) ) ;
#49877=CARTESIAN_POINT ( 'NONE',  ( -51.84221223720477667, -8.171052631578943348, 2.722470280083839178 ) ) ;
#49917=DIRECTION ( 'NONE',  ( -0.000000000000000000, 1.000000000000000000, 0.000000000000000000 ) ) ;
#49943=ORIENTED_EDGE ( 'NONE', *, *, #37637, .F. ) ;
#49948=CARTESIAN_POINT ( 'NONE',  ( -75.75000000000000000, 0.000000000000000000, 7.000000000000001776 ) ) ;
#49975=EDGE_CURVE ( 'NONE', #45120, #18574, #47268, .T. ) ;
#49996=CIRCLE ( 'NONE', #54428, 1.000000000000000000 ) ;
#50071=DIRECTION ( 'NONE',  ( 1.000000000000000000, 0.000000000000000000, 0.000000000000000000 ) ) ;
#50101=CARTESIAN_POINT ( 'NONE',  ( -83.49999999999998579, 4.336808689942018722E-16, 0.000000000000000000 ) ) ;
#50103=CARTESIAN_POINT ( 'NONE',  ( -12.74999999999999822, -4.000000000000000000, 7.000000000000001776 ) ) ;
#50105=CARTESIAN_POINT ( 'NONE',  ( -52.68151331240365920, -10.81621879791169150, 3.669590361806503775 ) ) ;
#50127=FACE_OUTER_BOUND ( 'NONE', #16610, .T. ) ;
#50146=FACE_OUTER_BOUND ( 'NONE', #13111, .T. ) ;
#50176=EDGE_CURVE ( 'NONE', #3393, #31013, #18340, .T. ) ;
#50224=CARTESIAN_POINT ( 'NONE',  ( -57.51969600708471830, 0.000000000000000000, -3.499999999999999112 ) ) ;
#50227=LINE ( 'NONE', #60405, #42826 ) ;
#50245=FACE_OUTER_BOUND ( 'NONE', #23571, .T. ) ;
#50278=CARTESIAN_POINT ( 'NONE',  ( -30.82866448558605299, -8.500000000000099476, -0.2278223570949065857 ) ) ;
#50283=CARTESIAN_POINT ( 'NONE',  ( -28.74999999999999645, -8.499999999999996447, 11.89999999999999680 ) ) ;
#50293=CARTESIAN_POINT ( 'NONE',  ( -59.14773785255846406, -8.499999999999992895, 0.8380523509896478096 ) ) ;
#50308=ORIENTED_EDGE ( 'NONE', *, *, #67041, .T. ) ;
#50317=CARTESIAN_POINT ( 'NONE',  ( -29.42522945561020364, -7.714901950938580555, -0.5387317027069097319 ) ) ;
#50324=AXIS2_PLACEMENT_3D ( 'NONE', #68448, #58935, #69478 ) ;
#50352=CARTESIAN_POINT ( 'NONE',  ( -49.99277014337361891, -10.94657273824542187, 3.697228369969763673 ) ) ;
#50404=DIRECTION ( 'NONE',  ( 0.000000000000000000, 0.000000000000000000, 1.000000000000000000 ) ) ;
#50408=CARTESIAN_POINT ( 'NONE',  ( -75.50000000000000000, -6.499999999999992006, 21.00000000000000000 ) ) ;
#50431=CARTESIAN_POINT ( 'NONE',  ( -54.25383070671073682, -8.228704836117380239, -2.000000000000000000 ) ) ;
#50434=CARTESIAN_POINT ( 'NONE',  ( -49.97293742689555529, -12.55532684748290784, 1.207170231723877718 ) ) ;
#50452=ORIENTED_EDGE ( 'NONE', *, *, #68734, .T. ) ;
#50481=CARTESIAN_POINT ( 'NONE',  ( -47.71347897792733761, -13.42724224818812040, 0.9185643661977238583 ) ) ;
#50493=CARTESIAN_POINT ( 'NONE',  ( -56.40813336638051112, -8.020529956771616398, -1.478673499587473295 ) ) ;
#50520=ORIENTED_EDGE ( 'NONE', *, *, #108, .F. ) ;
#50530=ORIENTED_EDGE ( 'NONE', *, *, #58282, .F. ) ;
#50564=VECTOR ( 'NONE', #35434, 1000.000000000000000 ) ;
#50567=COLOUR_RGB ( '', 0.31764706, 0.68627451, 0.89019608) ;
#50575=DIRECTION ( 'NONE',  ( -0.000000000000000000, 0.000000000000000000, -1.000000000000000000 ) ) ;
#50593=AXIS2_PLACEMENT_3D ( 'NONE', #37974, #21053, #42227 ) ;
#50659=DIRECTION ( 'NONE',  ( -0.000000000000000000, 1.000000000000000000, 0.000000000000000000 ) ) ;
#50690=EDGE_CURVE ( 'NONE', #3382, #63631, #6809, .T. ) ;
#50691=DIRECTION ( 'NONE',  ( 0.000000000000000000, 0.000000000000000000, 1.000000000000000000 ) ) ;
#50696=CARTESIAN_POINT ( 'NONE',  ( -32.35935878254957743, -8.628464621395343315, -2.363854359607545419 ) ) ;
#50755=EDGE_LOOP ( 'NONE', ( #32575, #19336, #45381, #30392, #56000, #1298, #7090, #9836, #66725, #56273, #22898, #21410, #10033, #62956, #4976, #64236, #44351, #57628 ) ) ;
#50783=CARTESIAN_POINT ( 'NONE',  ( -53.60138881051016568, -9.947368421052628307, 2.722470280083840066 ) ) ;
#50801=VECTOR ( 'NONE', #55210, 1000.000000000000000 ) ;
#50805=DIRECTION ( 'NONE',  ( 0.000000000000000000, 0.000000000000000000, -1.000000000000000000 ) ) ;
#50846=AXIS2_PLACEMENT_3D ( 'NONE', #54304, #21607, #43121 ) ;
#50865=ORIENTED_EDGE ( 'NONE', *, *, #28648, .F. ) ;
#50881=LINE ( 'NONE', #7607, #10414 ) ;
#50896=CARTESIAN_POINT ( 'NONE',  ( -37.98355297219490723, -12.77435968235000985, 2.829136785577898827 ) ) ;
#50965=CARTESIAN_POINT ( 'NONE',  ( -31.48711616987651141, -8.174231546256825354, -1.747660327496908916 ) ) ;
#50981=CARTESIAN_POINT ( 'NONE',  ( -27.86698944841959147, -8.499999999999998224, 0.009747179837370825370 ) ) ;
#51004=VERTEX_POINT ( 'NONE', #64797 ) ;
#51072=AXIS2_PLACEMENT_3D ( 'NONE', #9826, #41855, #25287 ) ;
#51117=VERTEX_POINT ( 'NONE', #27601 ) ;
#51163=EDGE_CURVE ( 'NONE', #51004, #26634, #22350, .T. ) ;
#51206=CIRCLE ( 'NONE', #20881, 1.000000000000000000 ) ;
#51217=ORIENTED_EDGE ( 'NONE', *, *, #46893, .T. ) ;
#51256=VECTOR ( 'NONE', #39203, 1000.000000000000000 ) ;
#51268=PLANE ( 'NONE',  #31618 ) ;
#51280=FACE_OUTER_BOUND ( 'NONE', #25844, .T. ) ;
#51289=CARTESIAN_POINT ( 'NONE',  ( -53.79830117337122175, -9.480064694306525652, -3.454096298679953048 ) ) ;
#51310=EDGE_LOOP ( 'NONE', ( #63472, #15645, #47722, #19146, #23795, #58763, #62834, #55880, #38767, #1115, #21218, #31750, #40107, #27864, #51217, #21543, #57266, #45346, #62504, #45426, #64433, #11150, #61238, #37747, #10466, #22946, #52509, #5796 ) ) ;
#51311=CARTESIAN_POINT ( 'NONE',  ( -29.91370621994246548, -7.761720733523306492, -0.7755720678496379472 ) ) ;
#51334=AXIS2_PLACEMENT_3D ( 'NONE', #65482, #54899, #6726 ) ;
#51371=DIRECTION ( 'NONE',  ( 1.000000000000000000, 0.000000000000000000, -0.000000000000000000 ) ) ;
#51378=CARTESIAN_POINT ( 'NONE',  ( -16.75000000000000000, -0.9999999999999995559, 19.00000000000000000 ) ) ;
#51393=CARTESIAN_POINT ( 'NONE',  ( -57.11974195712092239, -8.499999999999996447, 7.999999999999972466 ) ) ;
#51431=DIRECTION ( 'NONE',  ( 0.000000000000000000, 0.000000000000000000, 1.000000000000000000 ) ) ;
#51446=B_SPLINE_CURVE_WITH_KNOTS ( 'NONE', 3,
 ( #56301, #7446, #67214, #28869, #50352, #39832, #62285, #2079, #66527, #2443 ),
 .UNSPECIFIED., .F., .F.,
 ( 4, 2, 2, 2, 4 ),
 ( 0.000000000000000000, 0.001344558393249514153, 0.002689116786499028307, 0.004033675179748542894, 0.005378233572998056614 ),
 .UNSPECIFIED. ) ;
#51468=CARTESIAN_POINT ( 'NONE',  ( -8.921435019309294474E-16, -7.500000000000000888, 1.000000000000000000 ) ) ;
#51478=EDGE_CURVE ( 'NONE', #11986, #681, #21223, .T. ) ;
#51521=ORIENTED_EDGE ( 'NONE', *, *, #60236, .T. ) ;
#51527=LINE ( 'NONE', #19157, #63055 ) ;
#51559=VECTOR ( 'NONE', #19694, 1000.000000000000000 ) ;
#51572=FACE_OUTER_BOUND ( 'NONE', #42855, .T. ) ;
#51580=ORIENTED_EDGE ( 'NONE', *, *, #63399, .F. ) ;
#51592=CYLINDRICAL_SURFACE ( 'NONE', #57853, 1.000000000000000888 ) ;
#51601=VERTEX_POINT ( 'NONE', #221 ) ;
#51617=ORIENTED_EDGE ( 'NONE', *, *, #587, .T. ) ;
#51632=CARTESIAN_POINT ( 'NONE',  ( -53.64695261562590645, -9.497883372640860244, -3.722847864134625873 ) ) ;
#51647=( BOUNDED_CURVE ( )  B_SPLINE_CURVE ( 3, ( #27470, #32403, #1018, #43713 ),
 .UNSPECIFIED., .F., .F. ) 
 B_SPLINE_CURVE_WITH_KNOTS ( ( 4, 4 ),
 ( 1.570796326794896558, 2.351346768814403632 ),
 .UNSPECIFIED. ) 
 CURVE ( )  GEOMETRIC_REPRESENTATION_ITEM ( )  RATIONAL_B_SPLINE_CURVE ( ( 1.000000000000000000, 0.9498695926598446082, 0.9498695926598446082, 1.000000000000000000 ) ) 
 REPRESENTATION_ITEM ( '' )  );
#51653=VERTEX_POINT ( 'NONE', #50224 ) ;
#51656=VECTOR ( 'NONE', #6322, 1000.000000000000000 ) ;
#51690=CARTESIAN_POINT ( 'NONE',  ( 0.000000000000000000, 0.000000000000000000, 0.000000000000000000 ) ) ;
#51714=EDGE_CURVE ( 'NONE', #57439, #40317, #34789, .T. ) ;
#51754=CARTESIAN_POINT ( 'NONE',  ( -53.81525949776377615, -8.999709270181568854, 5.797011693762002871 ) ) ;
#51756=CARTESIAN_POINT ( 'NONE',  ( -10.74999999999999645, -0.9999999999999995559, 6.000000000000001776 ) ) ;
#51804=EDGE_CURVE ( 'NONE', #57528, #19277, #2669, .T. ) ;
#51805=ORIENTED_EDGE ( 'NONE', *, *, #8838, .T. ) ;
#51825=VERTEX_POINT ( 'NONE', #19583 ) ;
#51902=CARTESIAN_POINT ( 'NONE',  ( -58.06841298682653019, -7.714685904994091459, -0.5239124249552955526 ) ) ;
#51912=VERTEX_POINT ( 'NONE', #69503 ) ;
#52047=CARTESIAN_POINT ( 'NONE',  ( -33.24616929330141346, -8.228704836123991839, -2.000000000009505285 ) ) ;
#52051=ORIENTED_EDGE ( 'NONE', *, *, #58221, .F. ) ;
#52069=DIRECTION ( 'NONE',  ( -1.000000000000000000, -0.000000000000000000, -0.000000000000000000 ) ) ;
#52083=CARTESIAN_POINT ( 'NONE',  ( -87.50000000000000000, -6.499999999999990230, 21.00000000000000000 ) ) ;
#52112=CARTESIAN_POINT ( 'NONE',  ( -54.91675365088294569, -8.999709270181570631, 4.695517540642841325 ) ) ;
#52116=ORIENTED_EDGE ( 'NONE', *, *, #35180, .F. ) ;
#52127=ORIENTED_EDGE ( 'NONE', *, *, #46171, .T. ) ;
#52162=CARTESIAN_POINT ( 'NONE',  ( -60.70461754965442935, -7.499999999999993783, 2.168404344971008868E-16 ) ) ;
#52208=AXIS2_PLACEMENT_3D ( 'NONE', #17274, #27068, #37714 ) ;
#52234=CIRCLE ( 'NONE', #40992, 5.000000000000000000 ) ;
#52246=PLANE ( 'NONE',  #6961 ) ;
#52257=CARTESIAN_POINT ( 'NONE',  ( -30.38025804287905629, -8.499999999999996447, 0.06931351858032895608 ) ) ;
#52261=CARTESIAN_POINT ( 'NONE',  ( -37.71575249473459479, -12.64783167710381129, 1.172152365681724095 ) ) ;
#52290=ADVANCED_FACE ( 'NONE', ( #14579 ), #3998, .F. ) ;
#52296=EDGE_CURVE ( 'NONE', #39801, #53553, #41000, .T. ) ;
#52313=CARTESIAN_POINT ( 'NONE',  ( -40.19857555756883016, -13.54303449714841534, 2.705192303963718015 ) ) ;
#52339=DIRECTION ( 'NONE',  ( 0.000000000000000000, 0.000000000000000000, 1.000000000000000000 ) ) ;
#52347=ORIENTED_EDGE ( 'NONE', *, *, #27948, .T. ) ;
#52368=ADVANCED_FACE ( 'NONE', ( #4709 ), #51, .F. ) ;
#52404=DIRECTION ( 'NONE',  ( -0.000000000000000000, 0.000000000000000000, 1.000000000000000000 ) ) ;
#52413=AXIS2_PLACEMENT_3D ( 'NONE', #22047, #21005, #5844 ) ;
#52461=CARTESIAN_POINT ( 'NONE',  ( -55.81907424270178808, -8.628515624790351168, 6.048998428371599623 ) ) ;
#52483=DIRECTION ( 'NONE',  ( 0.7071067811865472397, 0.000000000000000000, -0.7071067811865477948 ) ) ;
#52509=ORIENTED_EDGE ( 'NONE', *, *, #68734, .F. ) ;
#52575=DIRECTION ( 'NONE',  ( 0.000000000000000000, 0.000000000000000000, 1.000000000000000000 ) ) ;
#52576=CARTESIAN_POINT ( 'NONE',  ( -83.49999999999998579, 4.336808689942018722E-16, -0.000000000000000000 ) ) ;
#52597=CIRCLE ( 'NONE', #57040, 2.500000000000002220 ) ;
#52607=CARTESIAN_POINT ( 'NONE',  ( -32.95000823261079859, -9.007918291183415249, 4.145374715402367904 ) ) ;
#52683=EDGE_CURVE ( 'NONE', #23192, #29467, #34717, .T. ) ;
#52697=CARTESIAN_POINT ( 'NONE',  ( -70.75000000000000000, -0.9999999999999995559, 24.00000000000000000 ) ) ;
#52746=FACE_OUTER_BOUND ( 'NONE', #54, .T. ) ;
#52747=ORIENTED_EDGE ( 'NONE', *, *, #6993, .T. ) ;
#52750=LINE ( 'NONE', #45604, #2686 ) ;
#52764=VERTEX_POINT ( 'NONE', #59456 ) ;
#52825=CARTESIAN_POINT ( 'NONE',  ( -43.75000000000000000, 0.000000000000000000, -7.000000000000000000 ) ) ;
#52842=EDGE_CURVE ( 'NONE', #51825, #47861, #25219, .T. ) ;
#52875=CARTESIAN_POINT ( 'NONE',  ( -54.73148258177910463, -9.107254030097815090, -2.000000000000000000 ) ) ;
#52891=ADVANCED_FACE ( 'NONE', ( #46372 ), #51268, .F. ) ;
#52922=AXIS2_PLACEMENT_3D ( 'NONE', #25288, #9483, #24245 ) ;
#52925=CARTESIAN_POINT ( 'NONE',  ( -11.74999999999999645, -0.9999999999999995559, 6.000000000000001776 ) ) ;
#52934=CARTESIAN_POINT ( 'NONE',  ( -32.76851741822840580, -9.107254030101904263, -2.000000000000000000 ) ) ;
#52937=ORIENTED_EDGE ( 'NONE', *, *, #60899, .F. ) ;
#52950=CARTESIAN_POINT ( 'NONE',  ( -69.74999999999998579, -4.000000000000000000, 24.00000000000000000 ) ) ;
#52967=ORIENTED_EDGE ( 'NONE', *, *, #58282, .T. ) ;
#52994=CARTESIAN_POINT ( 'NONE',  ( -32.56443198605217049, -8.762778093183483108, -2.500000000007921219 ) ) ;
#53032=AXIS2_PLACEMENT_3D ( 'NONE', #23307, #33182, #32828 ) ;
#53038=( NAMED_UNIT ( * ) PLANE_ANGLE_UNIT ( ) SI_UNIT ( $, .RADIAN. ) );
#53039=CARTESIAN_POINT ( 'NONE',  ( -32.87190215642332447, -9.152876382972353397, 4.262533829682994657 ) ) ;
#53062=EDGE_LOOP ( 'NONE', ( #23914, #5071, #4901, #27647 ) ) ;
#53063=CARTESIAN_POINT ( 'NONE',  ( -87.50000000000000000, -8.499999999999989342, 0.000000000000000000 ) ) ;
#53064=AXIS2_PLACEMENT_3D ( 'NONE', #22224, #28146, #66156 ) ;
#53111=DIRECTION ( 'NONE',  ( -1.000000000000000000, -0.000000000000000000, -0.000000000000000000 ) ) ;
#53147=CARTESIAN_POINT ( 'NONE',  ( -26.79538245034556709, -8.499999999999996447, 1.000000000000000000 ) ) ;
#53157=DIRECTION ( 'NONE',  ( 0.000000000000000000, 0.000000000000000000, 1.000000000000000000 ) ) ;
#53178=ORIENTED_EDGE ( 'NONE', *, *, #69683, .T. ) ;
#53182=AXIS2_PLACEMENT_3D ( 'NONE', #67529, #18658, #28838 ) ;
#53201=EDGE_LOOP ( 'NONE', ( #34809, #19524, #26118, #61915 ) ) ;
#53258=EDGE_CURVE ( 'NONE', #33018, #32747, #9999, .T. ) ;
#53264=DIRECTION ( 'NONE',  ( -0.000000000000000000, 1.000000000000000000, -0.000000000000000000 ) ) ;
#53278=AXIS2_PLACEMENT_3D ( 'NONE', #25853, #10044, #57530 ) ;
#53294=CARTESIAN_POINT ( 'NONE',  ( -75.75000000000000000, -3.000000000000000000, 19.00000000000000000 ) ) ;
#53323=ADVANCED_FACE ( 'NONE', ( #33514 ), #22268, .T. ) ;
#53351=CYLINDRICAL_SURFACE ( 'NONE', #42043, 1.000000000000000000 ) ;
#53359=DIRECTION ( 'NONE',  ( 1.000000000000000000, 0.000000000000000000, -0.000000000000000000 ) ) ;
#53405=ORIENTED_EDGE ( 'NONE', *, *, #49250, .F. ) ;
#53415=CARTESIAN_POINT ( 'NONE',  ( -40.24243276991634843, -11.80832556086091856, 3.294024383991729366 ) ) ;
#53427=ADVANCED_FACE ( 'NONE', ( #11360 ), #64831, .F. ) ;
#53447=ORIENTED_EDGE ( 'NONE', *, *, #45868, .T. ) ;
#53452=DIRECTION ( 'NONE',  ( -7.703719777548941223E-32, 1.000000000000000000, 0.000000000000000000 ) ) ;
#53470=DIRECTION ( 'NONE',  ( -1.000000000000000000, 0.000000000000000000, -0.000000000000000000 ) ) ;
#53476=VECTOR ( 'NONE', #12740, 1000.000000000000000 ) ;
#53520=CARTESIAN_POINT ( 'NONE',  ( -57.58629378005753097, -7.761720733523303828, -0.7755720678496390574 ) ) ;
#53533=EDGE_CURVE ( 'NONE', #23645, #42007, #23999, .T. ) ;
#53539=VERTEX_POINT ( 'NONE', #29625 ) ;
#53546=EDGE_CURVE ( 'NONE', #35999, #43029, #35043, .T. ) ;
#53553=VERTEX_POINT ( 'NONE', #24336 ) ;
#53582=( NAMED_UNIT ( * ) PLANE_ANGLE_UNIT ( ) SI_UNIT ( $, .RADIAN. ) );
#53588=CARTESIAN_POINT ( 'NONE',  ( -41.21370884129409973, -11.98618176148272241, 3.233652621117119708 ) ) ;
#53603=DIRECTION ( 'NONE',  ( -0.000000000000000000, -0.000000000000000000, -1.000000000000000000 ) ) ;
#53607=EDGE_CURVE ( 'NONE', #29847, #737, #64674, .T. ) ;
#53699=CYLINDRICAL_SURFACE ( 'NONE', #66611, 1.000000000000000000 ) ;
#53715=ORIENTED_EDGE ( 'NONE', *, *, #43019, .T. ) ;
#53745=EDGE_CURVE ( 'NONE', #42007, #54981, #50227, .T. ) ;
#53757=ORIENTED_EDGE ( 'NONE', *, *, #66891, .T. ) ;
#53758=PLANE ( 'NONE',  #15013 ) ;
#53784=DIRECTION ( 'NONE',  ( -1.000000000000000000, 0.000000000000000000, 0.000000000000000000 ) ) ;
#53786=ORIENTED_EDGE ( 'NONE', *, *, #36940, .F. ) ;
#53805=ORIENTED_EDGE ( 'NONE', *, *, #51478, .F. ) ;
#53830=FACE_OUTER_BOUND ( 'NONE', #25649, .T. ) ;
#53851=EDGE_LOOP ( 'NONE', ( #54958, #46432, #38771, #8574 ) ) ;
#53909=CARTESIAN_POINT ( 'NONE',  ( -32.76851741822989084, -9.107254030102708953, -2.000000000007038370 ) ) ;
#53927=PLANE ( 'NONE',  #475 ) ;
#54005=CARTESIAN_POINT ( 'NONE',  ( -7.731910350068054619E-16, -6.500000000000000888, 21.00000000000000000 ) ) ;
#54012=EDGE_CURVE ( 'NONE', #1406, #3527, #45131, .T. ) ;
#54038=ADVANCED_FACE ( 'NONE', ( #21308 ), #11457, .T. ) ;
#54050=ORIENTED_EDGE ( 'NONE', *, *, #47547, .F. ) ;
#54068=ADVANCED_FACE ( 'NONE', ( #37198 ), #48795, .T. ) ;
#54100=ORIENTED_EDGE ( 'NONE', *, *, #359, .T. ) ;
#54143=CARTESIAN_POINT ( 'NONE',  ( -43.24371837588274303, -14.00594677377896069, 0.7702318141522507267 ) ) ;
#54203=ORIENTED_EDGE ( 'NONE', *, *, #52296, .F. ) ;
#54223=EDGE_CURVE ( 'NONE', #5343, #17478, #12138, .T. ) ;
#54265=CARTESIAN_POINT ( 'NONE',  ( -42.80176904642062397, -12.14886544991757233, 3.185780282727390222 ) ) ;
#54282=VERTEX_POINT ( 'NONE', #29355 ) ;
#54304=CARTESIAN_POINT ( 'NONE',  ( -12.74999999999999822, -0.9999999999999995559, 7.000000000000001776 ) ) ;
#54335=ADVANCED_FACE ( 'NONE', ( #36051 ), #52246, .F. ) ;
#54358=VECTOR ( 'NONE', #21621, 1000.000000000000000 ) ;
#54365=VERTEX_POINT ( 'NONE', #46985 ) ;
#54369=AXIS2_PLACEMENT_3D ( 'NONE', #51468, #16211, #37686 ) ;
#54395=EDGE_CURVE ( 'NONE', #49493, #29467, #35193, .T. ) ;
#54421=CIRCLE ( 'NONE', #52208, 8.499999999999992895 ) ;
#54428=AXIS2_PLACEMENT_3D ( 'NONE', #13678, #35138, #29856 ) ;
#54441=LINE ( 'NONE', #44969, #50564 ) ;
#54448=ORIENTED_EDGE ( 'NONE', *, *, #36135, .T. ) ;
#54555=CARTESIAN_POINT ( 'NONE',  ( -55.11316530407558645, -8.908978040980905178, -2.125589934168188755 ) ) ;
#54558=CIRCLE ( 'NONE', #59086, 1.000000000000000000 ) ;
#54583=EDGE_CURVE ( 'NONE', #65886, #25898, #44666, .T. ) ;
#54598=VERTEX_POINT ( 'NONE', #60772 ) ;
#54622=FACE_OUTER_BOUND ( 'NONE', #68124, .T. ) ;
#54697=CARTESIAN_POINT ( 'NONE',  ( -51.46090993356868637, -11.68865663075333039, 1.590926122486572725 ) ) ;
#54703=ORIENTED_EDGE ( 'NONE', *, *, #19029, .F. ) ;
#54734=CARTESIAN_POINT ( 'NONE',  ( -30.38025804287907050, -8.500000000000000000, 7.999999999999983125 ) ) ;
#54762=AXIS2_PLACEMENT_3D ( 'NONE', #1875, #44203, #27938 ) ;
#54768=CIRCLE ( 'NONE', #63779, 1.000000000000000888 ) ;
#54795=EDGE_LOOP ( 'NONE', ( #35635, #59158, #45716, #55150 ) ) ;
#54840=VECTOR ( 'NONE', #58091, 1000.000000000000000 ) ;
#54857=ORIENTED_EDGE ( 'NONE', *, *, #3614, .T. ) ;
#54899=DIRECTION ( 'NONE',  ( -0.000000000000000000, -0.000000000000000000, 1.000000000000000000 ) ) ;
#54909=VERTEX_POINT ( 'NONE', #32090 ) ;
#54942=CARTESIAN_POINT ( 'NONE',  ( -43.33682035272221356, -12.17003437142647648, 3.180123757613341873 ) ) ;
#54951=ADVANCED_FACE ( 'NONE', ( #48302 ), #11318, .F. ) ;
#54958=ORIENTED_EDGE ( 'NONE', *, *, #44296, .T. ) ;
#54965=APPLICATION_CONTEXT ( 'automotive_design' ) ;
#54981=VERTEX_POINT ( 'NONE', #37423 ) ;
#54987=ORIENTED_EDGE ( 'NONE', *, *, #9401, .F. ) ;
#55006=CARTESIAN_POINT ( 'NONE',  ( -53.76864595461378826, -9.688118915545649301, -3.017821087588400619 ) ) ;
#55039=PRODUCT_DEFINITION_CONTEXT ( 'detailed design', #54965, 'design' ) ;
#55042=CYLINDRICAL_SURFACE ( 'NONE', #5628, 4.999999999999999112 ) ;
#55106=EDGE_LOOP ( 'NONE', ( #36086, #10539, #47741, #26768 ) ) ;
#55110=CARTESIAN_POINT ( 'NONE',  ( -37.47117118679384618, -12.53100696609209308, 2.887820269590780420 ) ) ;
#55148=VECTOR ( 'NONE', #47710, 1000.000000000000000 ) ;
#55150=ORIENTED_EDGE ( 'NONE', *, *, #9401, .T. ) ;
#55184=CARTESIAN_POINT ( 'NONE',  ( -53.60138881051016568, -9.947368421052624754, 2.722470280083841843 ) ) ;
#55208=CARTESIAN_POINT ( 'NONE',  ( -87.50000000000000000, -8.499999999999989342, 24.00000000000000000 ) ) ;
#55210=DIRECTION ( 'NONE',  ( 7.703719777548942317E-32, -1.000000000000000000, -0.000000000000000000 ) ) ;
#55216=B_SPLINE_CURVE_WITH_KNOTS ( 'NONE', 3,
 ( #37251, #4470, #19015, #40524, #20688, #42197 ),
 .UNSPECIFIED., .F., .F.,
 ( 4, 2, 4 ),
 ( 0.000000000000000000, 0.003161799692372087474, 0.006323599384744174948 ),
 .UNSPECIFIED. ) ;
#55224=CARTESIAN_POINT ( 'NONE',  ( -47.00571487472603849, -11.85301361210300897, 3.279042910798403820 ) ) ;
#55236=DIRECTION ( 'NONE',  ( 0.000000000000000000, 0.000000000000000000, -1.000000000000000000 ) ) ;
#55317=CARTESIAN_POINT ( 'NONE',  ( -43.75000000000000000, 0.000000000000000000, -2.000000000000000000 ) ) ;
#55330=ORIENTED_EDGE ( 'NONE', *, *, #56064, .T. ) ;
#55342=DIRECTION ( 'NONE',  ( -1.000000000000000000, 0.000000000000000000, 0.000000000000000000 ) ) ;
#55349=ORIENTED_EDGE ( 'NONE', *, *, #54012, .T. ) ;
#55357=CARTESIAN_POINT ( 'NONE',  ( -47.95907446719336775, -11.64228093534878994, 3.355646384069886246 ) ) ;
#55362=CLOSED_SHELL ( 'NONE', ( #31703, #66220, #44795, #32816, #59893, #43008, #37715, #10675, #48732, #44985, #42472, #60563, #3960, #54038, #16306, #30245, #16478, #38161, #11849, #58293, #57586, #10719, #3607, #36561, #44997, #5498, #41251, #58385, #36449, #45643, #49434, #15132, #13506, #54335, #48091, #41252, #59880, #4938, #27983, #47244, #53323, #16444, #52891, #63317, #44761, #46804, #30379, #45300, #42878, #7564, #27429, #5026, #67679, #45565, #27993, #10903, #60035, #69531, #64869, #52290, #52368, #19545, #14822, #9011, #3277, #14147, #57416, #54068, #55943, #33670, #3905, #27056, #60345, #20432, #23745, #8997, #46812, #1908, #53427, #36982, #65871, #43094, #67412, #32160, #35514, #39850, #54951 ) ) ;
#55398=CIRCLE ( 'NONE', #19445, 6.000000000000005329 ) ;
#55399=CARTESIAN_POINT ( 'NONE',  ( -56.25180925730852977, -8.571333231932012353, -0.5793937067663862406 ) ) ;
#55401=CARTESIAN_POINT ( 'NONE',  ( -53.60138881051016568, -9.947368421052624754, 2.722470280083841843 ) ) ;
#55424=FACE_OUTER_BOUND ( 'NONE', #54795, .T. ) ;
#55435=AXIS2_PLACEMENT_3D ( 'NONE', #41781, #50659, #45427 ) ;
#55461=ORIENTED_EDGE ( 'NONE', *, *, #7252, .T. ) ;
#55475=CARTESIAN_POINT ( 'NONE',  ( -34.83068933088741659, -10.82674371711464190, 3.661378181088279060 ) ) ;
#55500=ORIENTED_EDGE ( 'NONE', *, *, #26187, .F. ) ;
#55552=VECTOR ( 'NONE', #16699, 1000.000000000000000 ) ;
#55560=CARTESIAN_POINT ( 'NONE',  ( -29.49077592478069221, -8.499999999999996447, -0.3583504194180555102 ) ) ;
#55682=EDGE_CURVE ( 'NONE', #69054, #14523, #15757, .T. ) ;
#55710=CARTESIAN_POINT ( 'NONE',  ( -51.22377615987210930, -10.33468447027765791, 4.122506284637720064 ) ) ;
#55728=DIRECTION ( 'NONE',  ( -1.189524669241239115E-16, -1.000000000000000000, -0.000000000000000000 ) ) ;
#55775=CARTESIAN_POINT ( 'NONE',  ( -15.75000000000000000, -0.9999999999999995559, 19.00000000000000000 ) ) ;
#55818=CARTESIAN_POINT ( 'NONE',  ( -34.26930151262192936, -10.31448204818432579, 2.417974663400876079 ) ) ;
#55859=ORIENTED_EDGE ( 'NONE', *, *, #12000, .T. ) ;
#55866=FACE_OUTER_BOUND ( 'NONE', #39924, .T. ) ;
#55875=DIRECTION ( 'NONE',  ( 1.000000000000000000, 0.000000000000000000, 0.000000000000000000 ) ) ;
#55880=ORIENTED_EDGE ( 'NONE', *, *, #45184, .T. ) ;
#55889=CARTESIAN_POINT ( 'NONE',  ( -30.01048380477678990, -8.499999999999912959, -0.6003161102128471427 ) ) ;
#55914=CARTESIAN_POINT ( 'NONE',  ( -57.11974195712093660, -8.499999999999992895, 0.06931351858119066955 ) ) ;
#55943=ADVANCED_FACE ( 'NONE', ( #46684 ), #14624, .F. ) ;
#55956=CARTESIAN_POINT ( 'NONE',  ( -71.75000000000000000, -4.000000000000000000, 20.00000000000000000 ) ) ;
#56000=ORIENTED_EDGE ( 'NONE', *, *, #28394, .F. ) ;
#56058=FACE_OUTER_BOUND ( 'NONE', #34847, .T. ) ;
#56064=EDGE_CURVE ( 'NONE', #20404, #5343, #39223, .T. ) ;
#56114=ORIENTED_EDGE ( 'NONE', *, *, #20652, .F. ) ;
#56137=CARTESIAN_POINT ( 'NONE',  ( 0.000000000000000000, -3.500000000000000000, 24.00000000000000000 ) ) ;
#56152=CIRCLE ( 'NONE', #38232, 4.999999999999997335 ) ;
#56155=CARTESIAN_POINT ( 'NONE',  ( -36.85730689286826589, -10.63899366288961090, 3.897680902423376725 ) ) ;
#56164=MECHANICAL_DESIGN_GEOMETRIC_PRESENTATION_REPRESENTATION('',(#38247),#47299);
#56204=CIRCLE ( 'NONE', #21418, 13.99999999999999822 ) ;
#56240=CARTESIAN_POINT ( 'NONE',  ( -60.07797655783572566, -8.499999999999992895, 0.9794583065829002289 ) ) ;
#56273=ORIENTED_EDGE ( 'NONE', *, *, #66493, .T. ) ;
#56275=ORIENTED_EDGE ( 'NONE', *, *, #51163, .T. ) ;
#56301=CARTESIAN_POINT ( 'NONE',  ( -51.84221223720477667, -9.947368421052628307, 4.481646853389226415 ) ) ;
#56309=CARTESIAN_POINT ( 'NONE',  ( -84.49999999999998579, -2.499999999999999556, 0.000000000000000000 ) ) ;
#56387=VECTOR ( 'NONE', #11410, 1000.000000000000000 ) ;
#56389=DIRECTION ( 'NONE',  ( -0.000000000000000000, -1.000000000000000000, 0.000000000000000000 ) ) ;
#56391=CARTESIAN_POINT ( 'NONE',  ( -51.97253254664954625, -11.33456255750827602, 1.777144971367008441 ) ) ;
#56449=VERTEX_POINT ( 'NONE', #22640 ) ;
#56457=CARTESIAN_POINT ( 'NONE',  ( -49.75000000000000000, 2.168404344971008128E-16, -5.100000000000000533 ) ) ;
#56489=DIRECTION ( 'NONE',  ( 0.000000000000000000, 1.000000000000000000, 0.000000000000000000 ) ) ;
#56506=CARTESIAN_POINT ( 'NONE',  ( -40.70406133565712992, -11.89285714285713880, 3.265330863013268026 ) ) ;
#56535=ORIENTED_EDGE ( 'NONE', *, *, #45184, .F. ) ;
#56553=DIRECTION ( 'NONE',  ( -0.000000000000000000, 1.000000000000000000, -0.000000000000000000 ) ) ;
#56578=VERTEX_POINT ( 'NONE', #57064 ) ;
#56580=CARTESIAN_POINT ( 'NONE',  ( -31.70202421807500315, -8.271493738783197713, -1.899217192902302509 ) ) ;
#56609=CARTESIAN_POINT ( 'NONE',  ( -83.49999999999998579, 4.336808689942018722E-16, 24.00000000000000000 ) ) ;
#56613=DIRECTION ( 'NONE',  ( 0.000000000000000000, 0.000000000000000000, 1.000000000000000000 ) ) ;
#56641=ORIENTED_EDGE ( 'NONE', *, *, #1983, .F. ) ;
#56651=CARTESIAN_POINT ( 'NONE',  ( -11.74999999999999645, -0.9999999999999995559, 19.00000000000000000 ) ) ;
#56659=CIRCLE ( 'NONE', #26308, 1.000000000000000888 ) ;
#56667=DIRECTION ( 'NONE',  ( 0.000000000000000000, 0.000000000000000000, -1.000000000000000000 ) ) ;
#56684=CARTESIAN_POINT ( 'NONE',  ( -87.50000000000000000, -7.499999999999990230, 0.000000000000000000 ) ) ;
#56693=CARTESIAN_POINT ( 'NONE',  ( -32.85469148339993950, -8.952884650950863943, -2.692699799268927219 ) ) ;
#56716=EDGE_LOOP ( 'NONE', ( #2924, #66150, #35873 ) ) ;
#56738=ORIENTED_EDGE ( 'NONE', *, *, #63776, .T. ) ;
#56803=LINE ( 'NONE', #38145, #63302 ) ;
#56806=( NAMED_UNIT ( * ) SI_UNIT ( $, .STERADIAN. ) SOLID_ANGLE_UNIT ( ) );
#56807=CARTESIAN_POINT ( 'NONE',  ( -87.50000000000000000, -6.499999999999990230, 21.00000000000000000 ) ) ;
#56827=CARTESIAN_POINT ( 'NONE',  ( -74.75000000000000000, -0.9999999999999995559, 6.000000000000001776 ) ) ;
#56845=CARTESIAN_POINT ( 'NONE',  ( -57.11974195712093660, -7.499999999999993783, 0.06931351858119048914 ) ) ;
#56855=DIRECTION ( 'NONE',  ( 1.000000000000000000, 0.000000000000000000, 0.000000000000000000 ) ) ;
#56865=ORIENTED_EDGE ( 'NONE', *, *, #66785, .T. ) ;
#56882=EDGE_CURVE ( 'NONE', #21141, #38604, #25319, .T. ) ;
#56913=ORIENTED_EDGE ( 'NONE', *, *, #36089, .F. ) ;
#56959=DIRECTION ( 'NONE',  ( 1.000000000000000000, 0.000000000000000000, 0.000000000000000000 ) ) ;
#56986=( BOUNDED_CURVE ( )  B_SPLINE_CURVE ( 3, ( #69454, #31806, #26180, #21241 ),
 .UNSPECIFIED., .F., .F. ) 
 B_SPLINE_CURVE_WITH_KNOTS ( ( 4, 4 ),
 ( 4.712388980384689674, 6.283185307179586232 ),
 .UNSPECIFIED. ) 
 CURVE ( )  GEOMETRIC_REPRESENTATION_ITEM ( )  RATIONAL_B_SPLINE_CURVE ( ( 1.000000000000000000, 0.8047378541243649375, 0.8047378541243649375, 1.000000000000000000 ) ) 
 REPRESENTATION_ITEM ( '' )  );
#57040=AXIS2_PLACEMENT_3D ( 'NONE', #27327, #40889, #52483 ) ;
#57047=EDGE_LOOP ( 'NONE', ( #32076, #55349, #66749 ) ) ;
#57054=VECTOR ( 'NONE', #22610, 1000.000000000000000 ) ;
#57064=CARTESIAN_POINT ( 'NONE',  ( -74.75000000000000000, -4.000000000000000000, 7.000000000000001776 ) ) ;
#57101=EDGE_CURVE ( 'NONE', #56449, #43029, #36956, .T. ) ;
#57118=EDGE_CURVE ( 'NONE', #30231, #22278, #54558, .T. ) ;
#57129=DIRECTION ( 'NONE',  ( 1.000000000000000000, 0.000000000000000000, 0.000000000000000000 ) ) ;
#57144=VECTOR ( 'NONE', #58662, 1000.000000000000000 ) ;
#57183=DIRECTION ( 'NONE',  ( 0.000000000000000000, 0.000000000000000000, 1.000000000000000000 ) ) ;
#57202=EDGE_CURVE ( 'NONE', #54282, #54365, #35496, .T. ) ;
#57239=ORIENTED_EDGE ( 'NONE', *, *, #57355, .F. ) ;
#57249=EDGE_CURVE ( 'NONE', #6919, #32327, #43618, .T. ) ;
#57253=ORIENTED_EDGE ( 'NONE', *, *, #19994, .T. ) ;
#57266=ORIENTED_EDGE ( 'NONE', *, *, #11129, .F. ) ;
#57268=CARTESIAN_POINT ( 'NONE',  ( -11.33578643762689708, 3.244476573706588632E-16, 19.41421356237309581 ) ) ;
#57308=CARTESIAN_POINT ( 'NONE',  ( -83.49999999999998579, 4.336808689942018722E-16, 24.00000000000000000 ) ) ;
#57309=ORIENTED_EDGE ( 'NONE', *, *, #63776, .F. ) ;
#57355=EDGE_CURVE ( 'NONE', #51004, #54282, #46031, .T. ) ;
#57365=ORIENTED_EDGE ( 'NONE', *, *, #850, .T. ) ;
#57376=DIRECTION ( 'NONE',  ( 0.000000000000000000, 0.000000000000000000, 1.000000000000000000 ) ) ;
#57409=CARTESIAN_POINT ( 'NONE',  ( -59.44836694140673927, -8.499999999999992895, 0.9166795111384334893 ) ) ;
#57416=ADVANCED_FACE ( 'NONE', ( #51280 ), #36695, .F. ) ;
#57439=VERTEX_POINT ( 'NONE', #60278 ) ;
#57447=DIRECTION ( 'NONE',  ( 0.000000000000000000, 0.000000000000000000, 1.000000000000000000 ) ) ;
#57470=EDGE_CURVE ( 'NONE', #26721, #56578, #2900, .T. ) ;
#57485=CARTESIAN_POINT ( 'NONE',  ( -53.42422250819203100, -9.981287739266411663, -3.026606198070554754 ) ) ;
#57488=FILL_AREA_STYLE_COLOUR ( '', #50567 ) ;
#57503=EDGE_CURVE ( 'NONE', #35999, #17121, #69453, .T. ) ;
#57528=VERTEX_POINT ( 'NONE', #21967 ) ;
#57530=DIRECTION ( 'NONE',  ( 0.000000000000000000, 0.000000000000000000, -1.000000000000000000 ) ) ;
#57533=DIRECTION ( 'NONE',  ( 0.8753987966739757987, 0.000000000000000000, -0.4834014344018390252 ) ) ;
#57553=EDGE_CURVE ( 'NONE', #20590, #6919, #27249, .T. ) ;
#57586=ADVANCED_FACE ( 'NONE', ( #2522 ), #24279, .F. ) ;
#57590=DIRECTION ( 'NONE',  ( -0.000000000000000000, -0.000000000000000000, 1.000000000000000000 ) ) ;
#57616=FACE_OUTER_BOUND ( 'NONE', #59206, .T. ) ;
#57628=ORIENTED_EDGE ( 'NONE', *, *, #41423, .F. ) ;
#57632=ORIENTED_EDGE ( 'NONE', *, *, #4264, .T. ) ;
#57660=EDGE_CURVE ( 'NONE', #2398, #45832, #1474, .T. ) ;
#57750=CARTESIAN_POINT ( 'NONE',  ( -33.26911838175604430, -9.395153070120809247, -2.525443329778700008 ) ) ;
#57815=AXIS2_PLACEMENT_3D ( 'NONE', #45215, #6156, #44536 ) ;
#57846=CARTESIAN_POINT ( 'NONE',  ( -54.73148258177910463, -9.107254030097815090, -2.000000000000000000 ) ) ;
#57853=AXIS2_PLACEMENT_3D ( 'NONE', #47401, #35766, #3347 ) ;
#57939=CARTESIAN_POINT ( 'NONE',  ( -29.67263558057812389, -7.738202242605012771, -0.6497364857716234621 ) ) ;
#57972=AXIS2_PLACEMENT_3D ( 'NONE', #10206, #43308, #10551 ) ;
#57975=CARTESIAN_POINT ( 'NONE',  ( -33.41404910821478325, -9.512283121613517523, 3.449313401996988215 ) ) ;
#58006=CARTESIAN_POINT ( 'NONE',  ( -54.35505119478604286, -9.142989783843194829, -2.885398154219640965 ) ) ;
#58016=EDGE_CURVE ( 'NONE', #41095, #4575, #2802, .T. ) ;
#58023=DIRECTION ( 'NONE',  ( 0.2831056412805232902, 0.9590887320134375837, 0.000000000000000000 ) ) ;
#58072=CARTESIAN_POINT ( 'NONE',  ( -52.18882097621168725, -9.718525487687024622, 4.712719346062894665 ) ) ;
#58077=CARTESIAN_POINT ( 'NONE',  ( -75.50000000000000000, -8.499999999999991118, 21.00000000000000000 ) ) ;
#58091=DIRECTION ( 'NONE',  ( -0.000000000000000000, -0.000000000000000000, -1.000000000000000000 ) ) ;
#58126=( BOUNDED_CURVE ( )  B_SPLINE_CURVE ( 3, ( #40731, #42149, #63201, #4421 ),
 .UNSPECIFIED., .F., .F. ) 
 B_SPLINE_CURVE_WITH_KNOTS ( ( 4, 4 ),
 ( 3.141592653589793116, 4.712388980384689674 ),
 .UNSPECIFIED. ) 
 CURVE ( )  GEOMETRIC_REPRESENTATION_ITEM ( )  RATIONAL_B_SPLINE_CURVE ( ( 1.000000000000000000, 0.8047378541243649375, 0.8047378541243649375, 1.000000000000000000 ) ) 
 REPRESENTATION_ITEM ( '' )  );
#58180=CARTESIAN_POINT ( 'NONE',  ( -53.46164564159121113, -9.867047122144169791, -3.272593290840572600 ) ) ;
#58206=DIRECTION ( 'NONE',  ( 0.000000000000000000, 1.000000000000000000, 0.000000000000000000 ) ) ;
#58221=EDGE_CURVE ( 'NONE', #4254, #51004, #29920, .T. ) ;
#58222=EDGE_LOOP ( 'NONE', ( #3177, #24298, #40291, #27259, #2594 ) ) ;
#58224=ORIENTED_EDGE ( 'NONE', *, *, #69683, .F. ) ;
#58226=DIRECTION ( 'NONE',  ( -0.4834014344018414677, 0.000000000000000000, -0.8753987966739744664 ) ) ;
#58276=DIRECTION ( 'NONE',  ( -1.000000000000000000, -0.000000000000000000, -0.000000000000000000 ) ) ;
#58282=EDGE_CURVE ( 'NONE', #61550, #65886, #59075, .T. ) ;
#58293=ADVANCED_FACE ( 'NONE', ( #64353 ), #32123, .T. ) ;
#58302=CARTESIAN_POINT ( 'NONE',  ( -33.66753869681811295, -9.718525487688960851, 3.069079019093872152 ) ) ;
#58311=CARTESIAN_POINT ( 'NONE',  ( -58.75000000000000000, -4.000000000000000000, 18.10000000000000497 ) ) ;
#58320=CARTESIAN_POINT ( 'NONE',  ( -15.75000000000000000, 4.336808689942018722E-16, 20.00000000000000000 ) ) ;
#58340=AXIS2_PLACEMENT_3D ( 'NONE', #17717, #50404, #38853 ) ;
#58358=EDGE_CURVE ( 'NONE', #31013, #53539, #51206, .T. ) ;
#58385=ADVANCED_FACE ( 'NONE', ( #66422 ), #66783, .F. ) ;
#58412=AXIS2_PLACEMENT_3D ( 'NONE', #52825, #69000, #48615 ) ;
#58499=CARTESIAN_POINT ( 'NONE',  ( -71.75000000000000000, -0.9999999999999995559, 24.00000000000000000 ) ) ;
#58516=DIRECTION ( 'NONE',  ( -1.000000000000000000, 0.000000000000000000, -0.000000000000000000 ) ) ;
#58562=VECTOR ( 'NONE', #35573, 1000.000000000000000 ) ;
#58568=DIRECTION ( 'NONE',  ( 1.387778780781445676E-15, 0.000000000000000000, 1.000000000000000000 ) ) ;
#58578=ORIENTED_EDGE ( 'NONE', *, *, #31765, .F. ) ;
#58589=EDGE_LOOP ( 'NONE', ( #64766, #43294, #31639, #29272 ) ) ;
#58596=CARTESIAN_POINT ( 'NONE',  ( -43.75000000000000000, 0.000000000000000000, 0.000000000000000000 ) ) ;
#58652=CARTESIAN_POINT ( 'NONE',  ( -15.75000000000000000, -0.9999999999999995559, 20.00000000000000000 ) ) ;
#58662=DIRECTION ( 'NONE',  ( 0.000000000000000000, 0.000000000000000000, -1.000000000000000000 ) ) ;
#58669=CARTESIAN_POINT ( 'NONE',  ( -53.18756747357285519, -10.02680648607945102, -3.500000000000002220 ) ) ;
#58681=VECTOR ( 'NONE', #48126, 1000.000000000000000 ) ;
#58699=ORIENTED_EDGE ( 'NONE', *, *, #60899, .T. ) ;
#58716=VERTEX_POINT ( 'NONE', #17818 ) ;
#58733=CARTESIAN_POINT ( 'NONE',  ( -47.71347897792733761, -13.42724224818812040, 0.9185643661977238583 ) ) ;
#58763=ORIENTED_EDGE ( 'NONE', *, *, #50176, .T. ) ;
#58777=UNCERTAINTY_MEASURE_WITH_UNIT (LENGTH_MEASURE( 1.000000000000000082E-05 ), #24762, 'distance_accuracy_value', 'NONE');
#58805=DIRECTION ( 'NONE',  ( -0.000000000000000000, -0.000000000000000000, 1.000000000000000000 ) ) ;
#58855=B_SPLINE_CURVE_WITH_KNOTS ( 'NONE', 3,
 ( #2828, #56693, #25362, #45814, #36311, #14133 ),
 .UNSPECIFIED., .F., .F.,
 ( 4, 2, 4 ),
 ( 4.336808689942017736E-19, 0.001189544056195996052, 0.002379088112391991670 ),
 .UNSPECIFIED. ) ;
#58856=EDGE_CURVE ( 'NONE', #41095, #10826, #35730, .T. ) ;
#58877=CARTESIAN_POINT ( 'NONE',  ( -70.75000000000000000, -4.000000000000000000, 24.00000000000000000 ) ) ;
#58889=CARTESIAN_POINT ( 'NONE',  ( -4.000000000000000000, -3.499999999999999556, 24.00000000000000000 ) ) ;
#58897=CARTESIAN_POINT ( 'NONE',  ( -31.83594241490679622, -8.712327904965905034, -1.102500065259914619 ) ) ;
#58935=DIRECTION ( 'NONE',  ( -0.000000000000000000, 1.000000000000000000, -0.000000000000000000 ) ) ;
#58991=DIRECTION ( 'NONE',  ( -1.189524669241239855E-16, -1.000000000000000000, 0.000000000000000000 ) ) ;
#58994=CARTESIAN_POINT ( 'NONE',  ( -1.011095968855053334E-15, -8.500000000000000000, 3.000000000000000000 ) ) ;
#59009=CARTESIAN_POINT ( 'NONE',  ( -15.75000000000000000, -0.9999999999999995559, 19.00000000000000000 ) ) ;
#59075=CIRCLE ( 'NONE', #2845, 1.000000000000000888 ) ;
#59081=DIRECTION ( 'NONE',  ( 0.000000000000000000, 0.000000000000000000, 1.000000000000000000 ) ) ;
#59086=AXIS2_PLACEMENT_3D ( 'NONE', #10541, #31978, #53452 ) ;
#59113=VERTEX_POINT ( 'NONE', #9884 ) ;
#59134=CARTESIAN_POINT ( 'NONE',  ( -4.000000000000000000, 4.336808689942018722E-16, 24.00000000000000000 ) ) ;
#59154=DIRECTION ( 'NONE',  ( 0.000000000000000000, 0.000000000000000000, 1.000000000000000000 ) ) ;
#59158=ORIENTED_EDGE ( 'NONE', *, *, #26578, .T. ) ;
#59183=CIRCLE ( 'NONE', #51334, 1.000000000000000888 ) ;
#59185=CARTESIAN_POINT ( 'NONE',  ( -47.71347897792735182, -13.42724224818811862, 0.9185643661977266339 ) ) ;
#59190=CARTESIAN_POINT ( 'NONE',  ( 3.851859888774471706E-31, -8.500000000000000000, 24.00000000000000000 ) ) ;
#59193=FILL_AREA_STYLE_COLOUR ( '', #69689 ) ;
#59196=DIRECTION ( 'NONE',  ( -0.000000000000000000, 1.000000000000000000, 0.000000000000000000 ) ) ;
#59206=EDGE_LOOP ( 'NONE', ( #41838, #6127, #45898 ) ) ;
#59213=CARTESIAN_POINT ( 'NONE',  ( -17.75000000000000355, -3.000000000000000000, 24.00000000000000000 ) ) ;
#59231=AXIS2_PLACEMENT_3D ( 'NONE', #38712, #16207, #53470 ) ;
#59236=DIRECTION ( 'NONE',  ( 0.000000000000000000, -1.000000000000000000, -0.000000000000000000 ) ) ;
#59251=LINE ( 'NONE', #26559, #63969 ) ;
#59257=SPHERICAL_SURFACE ( 'NONE', #60362, 1.000000000000000000 ) ;
#59277=VECTOR ( 'NONE', #40723, 1000.000000000000000 ) ;
#59351=VERTEX_POINT ( 'NONE', #14019 ) ;
#59377=DIRECTION ( 'NONE',  ( 0.000000000000000000, 0.000000000000000000, 1.000000000000000000 ) ) ;
#59389=ORIENTED_EDGE ( 'NONE', *, *, #59538, .F. ) ;
#59407=CARTESIAN_POINT ( 'NONE',  ( -46.46084196965908575, -13.75011736874646395, 0.8310740330500354656 ) ) ;
#59454=DIRECTION ( 'NONE',  ( -1.000000000000000000, -0.000000000000000000, -0.000000000000000000 ) ) ;
#59456=CARTESIAN_POINT ( 'NONE',  ( -35.25000000000000000, 4.336808689942018722E-16, -5.099999999999999645 ) ) ;
#59511=CARTESIAN_POINT ( 'NONE',  ( -7.731910350068054619E-16, -6.500000000000000888, 21.00000000000000000 ) ) ;
#59515=CARTESIAN_POINT ( 'NONE',  ( -15.75000000000000000, 4.336808689942018722E-16, 24.00000000000000000 ) ) ;
#59538=EDGE_CURVE ( 'NONE', #17716, #20740, #6787, .T. ) ;
#59557=DIRECTION ( 'NONE',  ( -1.189524669241239115E-16, -1.000000000000000000, -0.000000000000000000 ) ) ;
#59566=EDGE_CURVE ( 'NONE', #26634, #49493, #35991, .T. ) ;
#59639=CARTESIAN_POINT ( 'NONE',  ( -69.74999999999998579, -3.000000000000000000, 0.000000000000000000 ) ) ;
#59660=EDGE_LOOP ( 'NONE', ( #25227, #52747, #34832, #66839 ) ) ;
#59683=VECTOR ( 'NONE', #20893, 1000.000000000000000 ) ;
#59691=CARTESIAN_POINT ( 'NONE',  ( -58.75000000000000000, -8.499999999999992895, 15.00000000000000178 ) ) ;
#59810=CIRCLE ( 'NONE', #27242, 2.499999999999999556 ) ;
#59859=CARTESIAN_POINT ( 'NONE',  ( -33.89861119020018521, -9.947368421756124235, -2.262137787255368515 ) ) ;
#59880=ADVANCED_FACE ( 'NONE', ( #36425 ), #31079, .F. ) ;
#59893=ADVANCED_FACE ( 'NONE', ( #26495 ), #20538, .T. ) ;
#59895=CARTESIAN_POINT ( 'NONE',  ( -47.00571487472603849, -11.85301361210301430, 3.279042910798484645 ) ) ;
#59977=CARTESIAN_POINT ( 'NONE',  ( 0.000000000000000000, 0.000000000000000000, 0.000000000000000000 ) ) ;
#59980=CARTESIAN_POINT ( 'NONE',  ( -15.75000000000000000, -0.9999999999999995559, 20.00000000000000000 ) ) ;
#59991=CARTESIAN_POINT ( 'NONE',  ( -87.50000000000000000, -3.500000000000000000, 0.000000000000000000 ) ) ;
#60002=ORIENTED_EDGE ( 'NONE', *, *, #43719, .F. ) ;
#60006=CARTESIAN_POINT ( 'NONE',  ( -11.74999999999999645, -4.000000000000000000, 6.000000000000001776 ) ) ;
#60009=CARTESIAN_POINT ( 'NONE',  ( -4.000000000000000000, -2.499999999999999556, 0.000000000000000000 ) ) ;
#60030=CARTESIAN_POINT ( 'NONE',  ( -31.35611772383057527, -8.500000000000001776, 7.349426879360468234 ) ) ;
#60035=ADVANCED_FACE ( 'NONE', ( #22616 ), #25235, .T. ) ;
#60072=VECTOR ( 'NONE', #59557, 1000.000000000000000 ) ;
#60109=CARTESIAN_POINT ( 'NONE',  ( -75.75000000000000000, -4.000000000000000000, 6.000000000000001776 ) ) ;
#60129=EDGE_LOOP ( 'NONE', ( #14117, #41759, #53715, #7365 ) ) ;
#60189=ORIENTED_EDGE ( 'NONE', *, *, #30594, .F. ) ;
#60207=ORIENTED_EDGE ( 'NONE', *, *, #49975, .F. ) ;
#60236=EDGE_CURVE ( 'NONE', #17125, #42263, #67564, .T. ) ;
#60243=CARTESIAN_POINT ( 'NONE',  ( -32.56443198605083467, -8.762778093182605588, -2.500000000007038370 ) ) ;
#60249=CARTESIAN_POINT ( 'NONE',  ( -45.19495320693604157, -13.94006660658549634, 0.7849218814955336576 ) ) ;
#60278=CARTESIAN_POINT ( 'NONE',  ( -28.74999999999999645, -4.000000000000000000, 18.10000000000000497 ) ) ;
#60302=CARTESIAN_POINT ( 'NONE',  ( -53.80170265663038265, -9.571662231010620303, -3.215428675398786407 ) ) ;
#60345=ADVANCED_FACE ( 'NONE', ( #28118 ), #32052, .T. ) ;
#60362=AXIS2_PLACEMENT_3D ( 'NONE', #16417, #63858, #68458 ) ;
#60385=ORIENTED_EDGE ( 'NONE', *, *, #56882, .T. ) ;
#60391=CARTESIAN_POINT ( 'NONE',  ( -37.45648088167604328, -10.91878729800595238, 3.716390883267106648 ) ) ;
#60405=CARTESIAN_POINT ( 'NONE',  ( -87.50000000000000000, -8.499999999999989342, 3.000000000000000000 ) ) ;
#60419=DIRECTION ( 'NONE',  ( 1.000000000000000000, -0.000000000000000000, 0.000000000000000000 ) ) ;
#60447=VECTOR ( 'NONE', #20539, 1000.000000000000000 ) ;
#60457=EDGE_LOOP ( 'NONE', ( #48062, #54448, #7419, #7779 ) ) ;
#60471=CARTESIAN_POINT ( 'NONE',  ( -27.33622931176552839, -7.538750321409861677, -3.015364001751804897E-16 ) ) ;
#60477=DIRECTION ( 'NONE',  ( -1.189524669241239115E-16, -1.000000000000000000, -0.000000000000000000 ) ) ;
#60506=CARTESIAN_POINT ( 'NONE',  ( -55.15277687475337842, -8.620516334094102007, -2.355797634318733458 ) ) ;
#60509=VERTEX_POINT ( 'NONE', #40821 ) ;
#60535=CARTESIAN_POINT ( 'NONE',  ( -83.49999999999998579, 4.336808689942018722E-16, -5.100000000000000533 ) ) ;
#60551=PLANE ( 'NONE',  #24642 ) ;
#60558=AXIS2_PLACEMENT_3D ( 'NONE', #43435, #33172, #48691 ) ;
#60563=ADVANCED_FACE ( 'NONE', ( #52746 ), #47507, .T. ) ;
#60580=CARTESIAN_POINT ( 'NONE',  ( 3.851859888774471706E-31, -8.500000000000000000, 24.00000000000000000 ) ) ;
#60589=ORIENTED_EDGE ( 'NONE', *, *, #53745, .T. ) ;
#60613=CARTESIAN_POINT ( 'NONE',  ( -53.24388477452971813, -10.30142299214062085, 2.428806256206293313 ) ) ;
#60649=CARTESIAN_POINT ( 'NONE',  ( -29.91370621994235890, -7.761720733523295834, -0.7755720678495816589 ) ) ;
#60704=ORIENTED_EDGE ( 'NONE', *, *, #30594, .T. ) ;
#60725=ORIENTED_EDGE ( 'NONE', *, *, #354, .F. ) ;
#60735=DIRECTION ( 'NONE',  ( 0.000000000000000000, -0.000000000000000000, -1.000000000000000000 ) ) ;
#60772=CARTESIAN_POINT ( 'NONE',  ( -51.84221223720477667, -9.947368421052628307, 4.481646853389226415 ) ) ;
#60783=ORIENTED_EDGE ( 'NONE', *, *, #21529, .T. ) ;
#60786=CYLINDRICAL_SURFACE ( 'NONE', #1477, 5.000000000000000888 ) ;
#60857=ORIENTED_EDGE ( 'NONE', *, *, #7483, .T. ) ;
#60899=EDGE_CURVE ( 'NONE', #24199, #2488, #58126, .T. ) ;
#60931=DIRECTION ( 'NONE',  ( -1.000000000000000000, 0.000000000000000000, -0.000000000000000000 ) ) ;
#60932=ORIENTED_EDGE ( 'NONE', *, *, #3664, .T. ) ;
#60954=DIRECTION ( 'NONE',  ( -0.000000000000000000, -0.000000000000000000, 1.000000000000000000 ) ) ;
#60965=CARTESIAN_POINT ( 'NONE',  ( -8.921435019309294474E-16, -7.500000000000000888, 1.000000000000000000 ) ) ;
#60967=CARTESIAN_POINT ( 'NONE',  ( -51.08064578546113665, -11.94071241913273518, 3.088929465764277627 ) ) ;
#61031=EDGE_CURVE ( 'NONE', #58716, #25360, #10070, .T. ) ;
#61094=CARTESIAN_POINT ( 'NONE',  ( -36.50190183960178558, -11.99078436789255164, 3.069443153576023153 ) ) ;
#61100=EDGE_CURVE ( 'NONE', #18574, #38604, #6508, .T. ) ;
#61134=ORIENTED_EDGE ( 'NONE', *, *, #25323, .F. ) ;
#61181=CARTESIAN_POINT ( 'NONE',  ( -27.32592744009309982, -8.499999999999996447, 0.03801221658426125888 ) ) ;
#61185=CIRCLE ( 'NONE', #37641, 13.76969600708472008 ) ;
#61205=CARTESIAN_POINT ( 'NONE',  ( -28.65793721421424323, -7.646217233412910375, -0.2644437612820810801 ) ) ;
#61238=ORIENTED_EDGE ( 'NONE', *, *, #29221, .F. ) ;
#61265=CARTESIAN_POINT ( 'NONE',  ( -43.75000000000000000, 4.336808689942018722E-16, -5.099999999999999645 ) ) ;
#61281=ORIENTED_EDGE ( 'NONE', *, *, #12860, .F. ) ;
#61321=CARTESIAN_POINT ( 'NONE',  ( -52.84851010692981532, -10.65464120701058803, 2.183759428457559437 ) ) ;
#61334=AXIS2_PLACEMENT_3D ( 'NONE', #34055, #65379, #44660 ) ;
#61347=EDGE_CURVE ( 'NONE', #20689, #62163, #55398, .T. ) ;
#61358=VECTOR ( 'NONE', #66153, 1000.000000000000000 ) ;
#61362=SHAPE_DEFINITION_REPRESENTATION ( #25409, #22166 ) ;
#61381=DIRECTION ( 'NONE',  ( 0.000000000000000000, -0.000000000000000000, 1.000000000000000000 ) ) ;
#61450=AXIS2_PLACEMENT_3D ( 'NONE', #2704, #56553, #23853 ) ;
#61500=FACE_OUTER_BOUND ( 'NONE', #62702, .T. ) ;
#61526=CIRCLE ( 'NONE', #24429, 1.000000000000000000 ) ;
#61550=VERTEX_POINT ( 'NONE', #25309 ) ;
#61640=ORIENTED_EDGE ( 'NONE', *, *, #50690, .F. ) ;
#61644=CYLINDRICAL_SURFACE ( 'NONE', #54369, 1.000000000000000000 ) ;
#61676=CARTESIAN_POINT ( 'NONE',  ( -34.31243252642735087, -10.02680648607962510, -3.499999999999997335 ) ) ;
#61695=SURFACE_STYLE_USAGE ( .BOTH. , #13885 ) ;
#61706=CIRCLE ( 'NONE', #29174, 1.999999999999999112 ) ;
#61720=AXIS2_PLACEMENT_3D ( 'NONE', #26828, #59196, #37823 ) ;
#61744=CARTESIAN_POINT ( 'NONE',  ( -83.49999999999998579, -3.499999999999999556, 24.00000000000000000 ) ) ;
#61785=DIRECTION ( 'NONE',  ( 0.000000000000000000, 1.000000000000000000, -0.000000000000000000 ) ) ;
#61832=DIRECTION ( 'NONE',  ( -0.000000000000000000, -0.000000000000000000, 1.000000000000000000 ) ) ;
#61915=ORIENTED_EDGE ( 'NONE', *, *, #34625, .F. ) ;
#61929=CARTESIAN_POINT ( 'NONE',  ( -53.60138881051016568, -9.947368421052630083, 2.722470280083837402 ) ) ;
#62043=LINE ( 'NONE', #31078, #25294 ) ;
#62163=VERTEX_POINT ( 'NONE', #56457 ) ;
#62199=CARTESIAN_POINT ( 'NONE',  ( -32.38698925772248316, -8.909055381080786873, -2.125700750517646398 ) ) ;
#62284=CARTESIAN_POINT ( 'NONE',  ( -30.41309959971616195, -7.810440804527638115, -1.036248593184375899 ) ) ;
#62285=CARTESIAN_POINT ( 'NONE',  ( -48.74730009840026668, -11.41203371166892744, 3.454827790524563014 ) ) ;
#62292=LINE ( 'NONE', #41555, #58562 ) ;
#62302=VERTEX_POINT ( 'NONE', #31802 ) ;
#62324=AXIS2_PLACEMENT_3D ( 'NONE', #14452, #35930, #57376 ) ;
#62336=DIRECTION ( 'NONE',  ( 0.000000000000000000, 0.000000000000000000, -1.000000000000000000 ) ) ;
#62361=EDGE_CURVE ( 'NONE', #1406, #40324, #42420, .T. ) ;
#62371=CARTESIAN_POINT ( 'NONE',  ( -34.75000000000000000, 0.000000000000000000, -2.000000000000000000 ) ) ;
#62504=ORIENTED_EDGE ( 'NONE', *, *, #42143, .F. ) ;
#62520=CARTESIAN_POINT ( 'NONE',  ( -53.91508968758270726, -9.466447511857611019, -3.170070218111717075 ) ) ;
#62621=DIRECTION ( 'NONE',  ( 1.000000000000000000, 0.000000000000000000, 0.000000000000000000 ) ) ;
#62641=DIRECTION ( 'NONE',  ( -1.000000000000000000, 1.445602896647339656E-16, 0.000000000000000000 ) ) ;
#62702=EDGE_LOOP ( 'NONE', ( #50308, #55500, #18363, #49226 ) ) ;
#62757=CARTESIAN_POINT ( 'NONE',  ( -17.75000000000000355, -4.000000000000000000, 0.000000000000000000 ) ) ;
#62764=DIRECTION ( 'NONE',  ( 0.000000000000000000, 0.000000000000000000, -1.000000000000000000 ) ) ;
#62788=FACE_OUTER_BOUND ( 'NONE', #34506, .T. ) ;
#62815=LINE ( 'NONE', #11351, #26888 ) ;
#62834=ORIENTED_EDGE ( 'NONE', *, *, #44604, .F. ) ;
#62865=SURFACE_SIDE_STYLE ('',( #47094 ) ) ;
#62910=PLANE ( 'NONE',  #23646 ) ;
#62920=EDGE_LOOP ( 'NONE', ( #39020, #6043, #26418, #31710 ) ) ;
#62956=ORIENTED_EDGE ( 'NONE', *, *, #33137, .T. ) ;
#62964=VERTEX_POINT ( 'NONE', #6225 ) ;
#62972=DIRECTION ( 'NONE',  ( 0.000000000000000000, 0.000000000000000000, -1.000000000000000000 ) ) ;
#63007=CARTESIAN_POINT ( 'NONE',  ( -34.03832277083918711, -9.867028709848661094, -3.272567082151741857 ) ) ;
#63021=CARTESIAN_POINT ( 'NONE',  ( -60.70461754965442935, -8.499999999999992895, 1.000000000000000222 ) ) ;
#63055=VECTOR ( 'NONE', #36063, 1000.000000000000000 ) ;
#63090=CARTESIAN_POINT ( 'NONE',  ( -11.99999999999999822, -6.499999999999999112, 3.000000000000000000 ) ) ;
#63093=VECTOR ( 'NONE', #32208, 1000.000000000000000 ) ;
#63100=DIRECTION ( 'NONE',  ( 0.000000000000000000, 0.000000000000000000, -1.000000000000000000 ) ) ;
#63132=CARTESIAN_POINT ( 'NONE',  ( -36.38551735505326690, -11.91035241884531182, 1.483988443825274617 ) ) ;
#63135=EDGE_CURVE ( 'NONE', #26634, #32528, #27830, .T. ) ;
#63137=CARTESIAN_POINT ( 'NONE',  ( -31.71532887107914789, -8.500000000000000000, 5.997393757699852834 ) ) ;
#63147=DIRECTION ( 'NONE',  ( 0.000000000000000000, 0.000000000000000000, 1.000000000000000000 ) ) ;
#63186=CIRCLE ( 'NONE', #32854, 1.000000000000000000 ) ;
#63190=AXIS2_PLACEMENT_3D ( 'NONE', #15185, #16216, #42965 ) ;
#63201=CARTESIAN_POINT ( 'NONE',  ( -75.33578643762689353, -4.000000000000000000, 18.58578643762690419 ) ) ;
#63271=VECTOR ( 'NONE', #37732, 1000.000000000000000 ) ;
#63276=FACE_OUTER_BOUND ( 'NONE', #51310, .T. ) ;
#63302=VECTOR ( 'NONE', #42745, 1000.000000000000000 ) ;
#63317=ADVANCED_FACE ( 'NONE', ( #4946 ), #8842, .F. ) ;
#63363=CARTESIAN_POINT ( 'NONE',  ( -33.02102729337801890, -9.244539245506066649, -2.264342667812435206 ) ) ;
#63373=VERTEX_POINT ( 'NONE', #68986 ) ;
#63388=ORIENTED_EDGE ( 'NONE', *, *, #66373, .F. ) ;
#63399=EDGE_CURVE ( 'NONE', #54282, #19551, #56659, .T. ) ;
#63427=ORIENTED_EDGE ( 'NONE', *, *, #10119, .T. ) ;
#63437=CARTESIAN_POINT ( 'NONE',  ( -4.000000000000000000, -2.499999999999999556, 24.00000000000000000 ) ) ;
#63448=( NAMED_UNIT ( * ) PLANE_ANGLE_UNIT ( ) SI_UNIT ( $, .RADIAN. ) );
#63465=VECTOR ( 'NONE', #127, 1000.000000000000000 ) ;
#63469=LINE ( 'NONE', #38154, #60072 ) ;
#63470=EDGE_CURVE ( 'NONE', #45684, #65886, #4978, .T. ) ;
#63472=ORIENTED_EDGE ( 'NONE', *, *, #19245, .T. ) ;
#63495=ORIENTED_EDGE ( 'NONE', *, *, #19245, .F. ) ;
#63533=CIRCLE ( 'NONE', #25318, 3.100000000000001865 ) ;
#63631=VERTEX_POINT ( 'NONE', #39073 ) ;
#63674=FACE_OUTER_BOUND ( 'NONE', #2049, .T. ) ;
#63739=CARTESIAN_POINT ( 'NONE',  ( -35.25000000000000000, 4.336808689942018722E-16, 0.000000000000000000 ) ) ;
#63776=EDGE_CURVE ( 'NONE', #36200, #2398, #49996, .T. ) ;
#63779=AXIS2_PLACEMENT_3D ( 'NONE', #66600, #55342, #41206 ) ;
#63793=FACE_BOUND ( 'NONE', #30323, .T. ) ;
#63823=ORIENTED_EDGE ( 'NONE', *, *, #51478, .T. ) ;
#63858=DIRECTION ( 'NONE',  ( 0.000000000000000000, 1.000000000000000000, 0.000000000000000000 ) ) ;
#63872=DIRECTION ( 'NONE',  ( 0.000000000000000000, 0.000000000000000000, -1.000000000000000000 ) ) ;
#63873=FACE_OUTER_BOUND ( 'NONE', #6229, .T. ) ;
#63874=DIRECTION ( 'NONE',  ( 0.000000000000000000, 0.000000000000000000, 1.000000000000000000 ) ) ;
#63890=VECTOR ( 'NONE', #69243, 1000.000000000000000 ) ;
#63895=FACE_OUTER_BOUND ( 'NONE', #48219, .T. ) ;
#63911=CARTESIAN_POINT ( 'NONE',  ( -34.93094464088179052, -9.512283121613265280, 4.966208934664647856 ) ) ;
#63917=LINE ( 'NONE', #64271, #30500 ) ;
#63964=VERTEX_POINT ( 'NONE', #18101 ) ;
#63969=VECTOR ( 'NONE', #31142, 1000.000000000000000 ) ;
#63987=ORIENTED_EDGE ( 'NONE', *, *, #3614, .F. ) ;
#63990=VECTOR ( 'NONE', #18715, 1000.000000000000000 ) ;
#64051=DIRECTION ( 'NONE',  ( 1.000000000000000000, 0.000000000000000000, 0.000000000000000000 ) ) ;
#64052=ORIENTED_EDGE ( 'NONE', *, *, #42237, .F. ) ;
#64128=CARTESIAN_POINT ( 'NONE',  ( -55.79276673654523933, -8.274029027338688280, -1.902897798319236777 ) ) ;
#64130=CARTESIAN_POINT ( 'NONE',  ( -87.50000000000000000, -6.499999999999990230, 3.000000000000000000 ) ) ;
#64156=CARTESIAN_POINT ( 'NONE',  ( -32.58426884830655013, -9.007081295888278660, -1.826937090823335108 ) ) ;
#64174=ORIENTED_EDGE ( 'NONE', *, *, #54223, .F. ) ;
#64177=( GEOMETRIC_REPRESENTATION_CONTEXT ( 3 ) GLOBAL_UNCERTAINTY_ASSIGNED_CONTEXT ( ( #20624 ) ) GLOBAL_UNIT_ASSIGNED_CONTEXT ( ( #24748, #63448, #31413 ) ) REPRESENTATION_CONTEXT ( 'NONE', 'WORKASPACE' ) );
#64184=CARTESIAN_POINT ( 'NONE',  ( -62.28939201416945082, 0.000000000000000000, -5.000000000000000000 ) ) ;
#64214=VECTOR ( 'NONE', #46946, 1000.000000000000000 ) ;
#64236=ORIENTED_EDGE ( 'NONE', *, *, #55682, .F. ) ;
#64237=CARTESIAN_POINT ( 'NONE',  ( -15.75000000000000000, -0.9999999999999995559, 24.00000000000000000 ) ) ;
#64239=EDGE_CURVE ( 'NONE', #20590, #51912, #19063, .T. ) ;
#64271=CARTESIAN_POINT ( 'NONE',  ( -87.50000000000000000, -6.499999999999990230, 21.00000000000000000 ) ) ;
#64285=LINE ( 'NONE', #37261, #57144 ) ;
#64309=VECTOR ( 'NONE', #27749, 1000.000000000000000 ) ;
#64319=EDGE_CURVE ( 'NONE', #26721, #19782, #15218, .T. ) ;
#64328=EDGE_LOOP ( 'NONE', ( #7761, #42563, #65040, #10418 ) ) ;
#64353=FACE_OUTER_BOUND ( 'NONE', #38024, .T. ) ;
#64372=CARTESIAN_POINT ( 'NONE',  ( -35.65778776279520912, -9.947368421052624754, 4.481646853389230856 ) ) ;
#64396=DIRECTION ( 'NONE',  ( 1.000000000000000000, 0.000000000000000000, 0.000000000000000000 ) ) ;
#64433=ORIENTED_EDGE ( 'NONE', *, *, #44225, .F. ) ;
#64464=ORIENTED_EDGE ( 'NONE', *, *, #51714, .F. ) ;
#64473=CARTESIAN_POINT ( 'NONE',  ( -57.11974195712093660, -8.499999999999992895, 8.000000000000000000 ) ) ;
#64496=CARTESIAN_POINT ( 'NONE',  ( -40.66238049145326272, -13.67042966192550502, 0.8504759240107299112 ) ) ;
#64522=ORIENTED_EDGE ( 'NONE', *, *, #30569, .T. ) ;
#64527=DIRECTION ( 'NONE',  ( 0.000000000000000000, 0.000000000000000000, -1.000000000000000000 ) ) ;
#64530=ORIENTED_EDGE ( 'NONE', *, *, #48565, .F. ) ;
#64584=CARTESIAN_POINT ( 'NONE',  ( -55.47019710162637551, -8.775703220318050057, -1.286986433361734461 ) ) ;
#64622=ORIENTED_EDGE ( 'NONE', *, *, #43407, .F. ) ;
#64647=CIRCLE ( 'NONE', #44501, 1.000000000000000888 ) ;
#64674=LINE ( 'NONE', #22445, #34941 ) ;
#64717=VECTOR ( 'NONE', #18227, 1000.000000000000000 ) ;
#64718=CARTESIAN_POINT ( 'NONE',  ( -44.54421273840488738, -13.99257275267859413, 0.7732724246005804325 ) ) ;
#64762=CARTESIAN_POINT ( 'NONE',  ( -11.74999999999999645, -4.000000000000000000, 19.00000000000000000 ) ) ;
#64766=ORIENTED_EDGE ( 'NONE', *, *, #39521, .T. ) ;
#64773=CARTESIAN_POINT ( 'NONE',  ( -56.67071223451711859, -8.499999999999992895, -0.2282353707497825623 ) ) ;
#64791=ORIENTED_EDGE ( 'NONE', *, *, #29221, .T. ) ;
#64792=FACE_OUTER_BOUND ( 'NONE', #56716, .T. ) ;
#64797=CARTESIAN_POINT ( 'NONE',  ( -16.75000000000000000, -0.9999999999999995559, 20.00000000000000000 ) ) ;
#64811=FACE_OUTER_BOUND ( 'NONE', #43886, .T. ) ;
#64831=SPHERICAL_SURFACE ( 'NONE', #40695, 1.000000000000000000 ) ;
#64869=ADVANCED_FACE ( 'NONE', ( #57616 ), #4686, .T. ) ;
#64904=DIRECTION ( 'NONE',  ( 0.000000000000000000, 0.000000000000000000, -1.000000000000000000 ) ) ;
#64915=DIRECTION ( 'NONE',  ( 0.000000000000000000, -0.000000000000000000, 1.000000000000000000 ) ) ;
#64932=DIRECTION ( 'NONE',  ( 0.000000000000000000, 0.000000000000000000, -1.000000000000000000 ) ) ;
#64983=DIRECTION ( 'NONE',  ( -0.7071067811865483499, 0.000000000000000000, -0.7071067811865466846 ) ) ;
#65007=ORIENTED_EDGE ( 'NONE', *, *, #44296, .F. ) ;
#65018=ORIENTED_EDGE ( 'NONE', *, *, #58221, .T. ) ;
#65024=CARTESIAN_POINT ( 'NONE',  ( -54.73909730288738018, -9.103122581846379902, -2.000000000000000000 ) ) ;
#65029=CARTESIAN_POINT ( 'NONE',  ( -74.75000000000000000, -3.000000000000000000, 0.000000000000000000 ) ) ;
#65040=ORIENTED_EDGE ( 'NONE', *, *, #26897, .F. ) ;
#65167=CARTESIAN_POINT ( 'NONE',  ( -46.35633800517990011, -13.76932876361770752, 2.685086742506573199 ) ) ;
#65193=AXIS2_PLACEMENT_3D ( 'NONE', #6334, #66834, #40121 ) ;
#65232=ORIENTED_EDGE ( 'NONE', *, *, #21342, .T. ) ;
#65244=ORIENTED_EDGE ( 'NONE', *, *, #14084, .F. ) ;
#65256=VECTOR ( 'NONE', #15230, 1000.000000000000000 ) ;
#65265=VECTOR ( 'NONE', #61785, 1000.000000000000000 ) ;
#65268=EDGE_CURVE ( 'NONE', #19277, #23284, #16392, .T. ) ;
#65347=ORIENTED_EDGE ( 'NONE', *, *, #354, .T. ) ;
#65371=EDGE_LOOP ( 'NONE', ( #51805, #27912, #12322 ) ) ;
#65379=DIRECTION ( 'NONE',  ( 0.000000000000000000, -0.000000000000000000, -1.000000000000000000 ) ) ;
#65399=FACE_OUTER_BOUND ( 'NONE', #2852, .T. ) ;
#65420=CARTESIAN_POINT ( 'NONE',  ( -29.82215890055010377, -8.499999999999996447, 0.3549037236123264716 ) ) ;
#65454=TOROIDAL_SURFACE ( 'NONE', #50846, 2.000000000000000000, 1.000000000000000000 ) ;
#65464=CARTESIAN_POINT ( 'NONE',  ( -55.95931559381303089, -8.622190103400207306, -1.508108381079090510 ) ) ;
#65482=CARTESIAN_POINT ( 'NONE',  ( -10.74999999999999645, -0.9999999999999995559, 7.000000000000001776 ) ) ;
#65524=CARTESIAN_POINT ( 'NONE',  ( -40.19857555756881595, -13.54303449714841889, 2.705192303963717126 ) ) ;
#65545=VECTOR ( 'NONE', #60954, 1000.000000000000000 ) ;
#65557=FACE_OUTER_BOUND ( 'NONE', #5224, .T. ) ;
#65565=ORIENTED_EDGE ( 'NONE', *, *, #49656, .T. ) ;
#65614=B_SPLINE_CURVE_WITH_KNOTS ( 'NONE', 3,
 ( #47715, #14971, #47002, #16018, #9335, #31447, #63132, #25150, #52261, #47346, #15657, #69451 ),
 .UNSPECIFIED., .F., .F.,
 ( 4, 2, 2, 2, 2, 4 ),
 ( 4.336808689942017255E-19, 0.001855247662732223239, 0.002782871494098332690, 0.003710495325464443009, 0.005565742988196644564, 0.007420990650928846986 ),
 .UNSPECIFIED. ) ;
#65638=AXIS2_PLACEMENT_3D ( 'NONE', #23751, #8625, #67024 ) ;
#65700=VECTOR ( 'NONE', #5748, 1000.000000000000000 ) ;
#65714=EDGE_LOOP ( 'NONE', ( #6271, #59389 ) ) ;
#65739=VECTOR ( 'NONE', #60419, 1000.000000000000000 ) ;
#65815=CARTESIAN_POINT ( 'NONE',  ( -54.91578578071454331, -9.007051595042142367, -1.826885762205050501 ) ) ;
#65867=CARTESIAN_POINT ( 'NONE',  ( -33.24469977103449736, -9.366146070812339630, -2.498496608837086796 ) ) ;
#65871=ADVANCED_FACE ( 'NONE', ( #42202 ), #48496, .T. ) ;
#65886=VERTEX_POINT ( 'NONE', #20331 ) ;
#65914=ORIENTED_EDGE ( 'NONE', *, *, #13743, .T. ) ;
#65948=CARTESIAN_POINT ( 'NONE',  ( -58.75000000000000000, -13.99999999999999822, 11.89999999999999858 ) ) ;
#65954=CARTESIAN_POINT ( 'NONE',  ( -54.91569865845073650, -9.007098961898055478, -1.826967611413356396 ) ) ;
#65976=AXIS2_PLACEMENT_3D ( 'NONE', #48922, #5592, #59081 ) ;
#66022=CARTESIAN_POINT ( 'NONE',  ( -38.83454371628977242, -13.12359704688498141, 1.007153542399198409 ) ) ;
#66038=ORIENTED_EDGE ( 'NONE', *, *, #12469, .T. ) ;
#66054=EDGE_LOOP ( 'NONE', ( #46394, #38758, #10947, #20044, #68530, #52347, #26935, #40601, #67531, #39220 ) ) ;
#66059=CARTESIAN_POINT ( 'NONE',  ( -75.75000000000000000, -0.9999999999999995559, 19.00000000000000000 ) ) ;
#66081=LINE ( 'NONE', #49238, #66603 ) ;
#66150=ORIENTED_EDGE ( 'NONE', *, *, #64239, .T. ) ;
#66153=DIRECTION ( 'NONE',  ( 1.000000000000000000, -0.000000000000000000, -0.000000000000000000 ) ) ;
#66156=DIRECTION ( 'NONE',  ( 1.000000000000000000, 0.000000000000000000, 0.000000000000000000 ) ) ;
#66160=EDGE_LOOP ( 'NONE', ( #47526, #49651, #39906, #65018 ) ) ;
#66179=CARTESIAN_POINT ( 'NONE',  ( -71.75000000000000000, -3.000000000000000000, 18.00000000000000000 ) ) ;
#66197=CIRCLE ( 'NONE', #3247, 1.000000000000000888 ) ;
#66202=ORIENTED_EDGE ( 'NONE', *, *, #51714, .T. ) ;
#66212=AXIS2_PLACEMENT_3D ( 'NONE', #41420, #35069, #13604 ) ;
#66220=ADVANCED_FACE ( 'NONE', ( #25519 ), #48076, .F. ) ;
#66250=CARTESIAN_POINT ( 'NONE',  ( -48.63607860962903828, -13.13395492442522539, 2.757111910427318513 ) ) ;
#66283=DIRECTION ( 'NONE',  ( -0.000000000000000000, -1.000000000000000000, -0.000000000000000000 ) ) ;
#66373=EDGE_CURVE ( 'NONE', #48775, #20367, #31486, .T. ) ;
#66384=VERTEX_POINT ( 'NONE', #37877 ) ;
#66407=CARTESIAN_POINT ( 'NONE',  ( -33.89861118948982721, -9.947368421052626530, -7.000000000000000000 ) ) ;
#66412=AXIS2_PLACEMENT_3D ( 'NONE', #32550, #15719, #36847 ) ;
#66422=FACE_OUTER_BOUND ( 'NONE', #38459, .T. ) ;
#66442=CARTESIAN_POINT ( 'NONE',  ( -31.83028512801498877, -8.710578351985672541, -1.097192391871058437 ) ) ;
#66458=CARTESIAN_POINT ( 'NONE',  ( -29.24174177788027507, -8.499999999999996447, 0.6065382340992577781 ) ) ;
#66493=EDGE_CURVE ( 'NONE', #13277, #57528, #12807, .T. ) ;
#66526=CARTESIAN_POINT ( 'NONE',  ( -29.91370621994235890, -7.761720733523295834, -0.7755720678495816589 ) ) ;
#66527=CARTESIAN_POINT ( 'NONE',  ( -47.44854201893517143, -11.76587057138590886, 3.309444246618569174 ) ) ;
#66550=CARTESIAN_POINT ( 'NONE',  ( -84.49999999999998579, -2.499999999999999556, 24.00000000000000000 ) ) ;
#66565=LINE ( 'NONE', #49702, #53476 ) ;
#66570=DIRECTION ( 'NONE',  ( -1.189524669241239115E-16, -1.000000000000000000, -0.000000000000000000 ) ) ;
#66572=B_SPLINE_CURVE_WITH_KNOTS ( 'NONE', 3,
 ( #45403, #34103, #56240, #66824, #50293, #17610, #2013, #40112 ),
 .UNSPECIFIED., .F., .F.,
 ( 4, 2, 2, 4 ),
 ( 0.000000000000000000, 0.0009392049334771340394, 0.001878409866954268079, 0.003756819733908536157 ),
 .UNSPECIFIED. ) ;
#66577=DIRECTION ( 'NONE',  ( 0.000000000000000000, 0.000000000000000000, 1.000000000000000000 ) ) ;
#66600=CARTESIAN_POINT ( 'NONE',  ( -87.50000000000000000, -7.499999999999990230, 23.00000000000000000 ) ) ;
#66603=VECTOR ( 'NONE', #17908, 1000.000000000000000 ) ;
#66611=AXIS2_PLACEMENT_3D ( 'NONE', #50103, #18075, #1832 ) ;
#66616=CARTESIAN_POINT ( 'NONE',  ( -48.86169860080597971, -11.37553613063878366, 3.471446820368512043 ) ) ;
#66634=DIRECTION ( 'NONE',  ( 1.000000000000000000, 0.000000000000000000, 0.000000000000000000 ) ) ;
#66662=CARTESIAN_POINT ( 'NONE',  ( -51.21480343399456814, -11.84745778642585989, 1.513780993297752175 ) ) ;
#66664=DIRECTION ( 'NONE',  ( 0.000000000000000000, 0.000000000000000000, -1.000000000000000000 ) ) ;
#66710=DIRECTION ( 'NONE',  ( 0.000000000000000000, 0.000000000000000000, 1.000000000000000000 ) ) ;
#66725=ORIENTED_EDGE ( 'NONE', *, *, #27388, .T. ) ;
#66749=ORIENTED_EDGE ( 'NONE', *, *, #4264, .F. ) ;
#66752=DIRECTION ( 'NONE',  ( -0.000000000000000000, 1.000000000000000000, -0.000000000000000000 ) ) ;
#66779=CARTESIAN_POINT ( 'NONE',  ( -54.52476335569559041, -9.117691409003279901, -3.352975844306524511 ) ) ;
#66781=VECTOR ( 'NONE', #48976, 1000.000000000000000 ) ;
#66783=PLANE ( 'NONE',  #16389 ) ;
#66784=ORIENTED_EDGE ( 'NONE', *, *, #29447, .T. ) ;
#66785=EDGE_CURVE ( 'NONE', #13126, #20404, #24322, .T. ) ;
#66808=AXIS2_PLACEMENT_3D ( 'NONE', #10236, #31313, #46524 ) ;
#66824=CARTESIAN_POINT ( 'NONE',  ( -59.45644908980804644, -8.499999999999992895, 0.8985947643278344721 ) ) ;
#66834=DIRECTION ( 'NONE',  ( -1.445602896647339656E-16, -1.000000000000000000, 0.000000000000000000 ) ) ;
#66839=ORIENTED_EDGE ( 'NONE', *, *, #53546, .T. ) ;
#66891=EDGE_CURVE ( 'NONE', #51825, #41337, #30204, .T. ) ;
#66970=CARTESIAN_POINT ( 'NONE',  ( -49.91467138050326469, -10.97405843795318070, 3.683894230925336633 ) ) ;
#67024=DIRECTION ( 'NONE',  ( -1.000000000000000000, 0.000000000000000000, 0.000000000000000000 ) ) ;
#67041=EDGE_CURVE ( 'NONE', #14317, #35896, #61526, .T. ) ;
#67053=EDGE_CURVE ( 'NONE', #18813, #32327, #52597, .T. ) ;
#67081=UNCERTAINTY_MEASURE_WITH_UNIT (LENGTH_MEASURE( 1.000000000000000082E-05 ), #48697, 'distance_accuracy_value', 'NONE');
#67115=ORIENTED_EDGE ( 'NONE', *, *, #56882, .F. ) ;
#67122=ORIENTED_EDGE ( 'NONE', *, *, #24509, .F. ) ;
#67133=ORIENTED_EDGE ( 'NONE', *, *, #5230, .F. ) ;
#67137=CARTESIAN_POINT ( 'NONE',  ( -30.38818854855176355, -7.808010524275851516, -1.023245363186933155 ) ) ;
#67209=EDGE_LOOP ( 'NONE', ( #63823, #54050, #34681, #64052 ) ) ;
#67213=CARTESIAN_POINT ( 'NONE',  ( -31.73356630351995733, -8.286794552894653165, -1.921513618645009913 ) ) ;
#67214=CARTESIAN_POINT ( 'NONE',  ( -51.15237142740936349, -10.37588836492439448, 4.088776396995604578 ) ) ;
#67381=LINE ( 'NONE', #24799, #35729 ) ;
#67402=DIRECTION ( 'NONE',  ( 0.000000000000000000, 0.000000000000000000, -1.000000000000000000 ) ) ;
#67412=ADVANCED_FACE ( 'NONE', ( #47765 ), #59257, .T. ) ;
#67480=FACE_OUTER_BOUND ( 'NONE', #847, .T. ) ;
#67529=CARTESIAN_POINT ( 'NONE',  ( -69.74999999999998579, -3.000000000000000000, 24.00000000000000000 ) ) ;
#67531=ORIENTED_EDGE ( 'NONE', *, *, #49250, .T. ) ;
#67554=AXIS2_PLACEMENT_3D ( 'NONE', #56309, #12349, #29223 ) ;
#67563=CARTESIAN_POINT ( 'NONE',  ( -11.74999999999999645, -3.000000000000000000, 19.00000000000000000 ) ) ;
#67564=CIRCLE ( 'NONE', #7998, 3.100000000000003642 ) ;
#67637=VECTOR ( 'NONE', #66570, 1000.000000000000000 ) ;
#67649=CARTESIAN_POINT ( 'NONE',  ( -15.75000000000000000, -4.000000000000000000, 19.00000000000000000 ) ) ;
#67651=FACE_OUTER_BOUND ( 'NONE', #47105, .T. ) ;
#67679=ADVANCED_FACE ( 'NONE', ( #7122 ), #28909, .T. ) ;
#67682=EDGE_CURVE ( 'NONE', #24916, #14317, #397, .T. ) ;
#67703=DIRECTION ( 'NONE',  ( 0.000000000000000000, 0.000000000000000000, 1.000000000000000000 ) ) ;
#67766=CARTESIAN_POINT ( 'NONE',  ( -87.50000000000000000, -3.500000000000000000, 24.00000000000000000 ) ) ;
#67794=CARTESIAN_POINT ( 'NONE',  ( -75.50000000000000000, -6.499999999999992006, 21.00000000000000000 ) ) ;
#67796=VECTOR ( 'NONE', #37613, 1000.000000000000000 ) ;
#67818=CARTESIAN_POINT ( 'NONE',  ( -53.18268485490532527, -10.02774732068181507, -3.508434557029057821 ) ) ;
#67828=FILL_AREA_STYLE_COLOUR ( '', #18896 ) ;
#67887=( BOUNDED_CURVE ( )  B_SPLINE_CURVE ( 3, ( #19528, #8991, #45625, #13552 ),
 .UNSPECIFIED., .F., .F. ) 
 B_SPLINE_CURVE_WITH_KNOTS ( ( 4, 4 ),
 ( 3.931838538365183489, 4.712388980384689674 ),
 .UNSPECIFIED. ) 
 CURVE ( )  GEOMETRIC_REPRESENTATION_ITEM ( )  RATIONAL_B_SPLINE_CURVE ( ( 1.000000000000000000, 0.9498695926598449413, 0.9498695926598449413, 1.000000000000000000 ) ) 
 REPRESENTATION_ITEM ( '' )  );
#67906=PRODUCT_DEFINITION ( 'UNKNOWN', '', #11305, #55039 ) ;
#67942=VECTOR ( 'NONE', #33989, 1000.000000000000000 ) ;
#67956=AXIS2_PLACEMENT_3D ( 'NONE', #39003, #60735, #7629 ) ;
#67984=CARTESIAN_POINT ( 'NONE',  ( -60.07898600000864775, -8.499999999999992895, 0.9999999981295574214 ) ) ;
#67985=ORIENTED_EDGE ( 'NONE', *, *, #24679, .T. ) ;
#68034=CARTESIAN_POINT ( 'NONE',  ( -87.50000000000000000, -8.499999999999989342, 24.00000000000000000 ) ) ;
#68055=CARTESIAN_POINT ( 'NONE',  ( -54.47897255799113481, -9.244539326313761407, -2.264342823408200367 ) ) ;
#68086=CARTESIAN_POINT ( 'NONE',  ( -60.43227690047157807, -7.519512524622562033, 4.573977915173213819E-17 ) ) ;
#68090=CARTESIAN_POINT ( 'NONE',  ( -87.50000000000000000, -6.499999999999990230, 3.000000000000000000 ) ) ;
#68111=CIRCLE ( 'NONE', #25402, 1.000000000000000000 ) ;
#68124=EDGE_LOOP ( 'NONE', ( #38937, #52967, #366, #19937 ) ) ;
#68182=CARTESIAN_POINT ( 'NONE',  ( -33.08284415674632584, -9.238994630453197132, 5.297413886133312211 ) ) ;
#68185=VECTOR ( 'NONE', #64932, 1000.000000000000000 ) ;
#68222=CARTESIAN_POINT ( 'NONE',  ( -47.00571487472603138, -11.02952041815452766, 0.9185643661977246355 ) ) ;
#68249=ORIENTED_EDGE ( 'NONE', *, *, #58016, .T. ) ;
#68272=PLANE ( 'NONE',  #3481 ) ;
#68335=ORIENTED_EDGE ( 'NONE', *, *, #37138, .F. ) ;
#68341=ORIENTED_EDGE ( 'NONE', *, *, #59566, .T. ) ;
#68381=EDGE_CURVE ( 'NONE', #30219, #38604, #64285, .T. ) ;
#68448=CARTESIAN_POINT ( 'NONE',  ( -28.74999999999999645, -13.99999999999999822, 15.00000000000000178 ) ) ;
#68458=DIRECTION ( 'NONE',  ( 1.000000000000000000, 0.000000000000000000, 0.000000000000000000 ) ) ;
#68518=( LENGTH_UNIT ( ) NAMED_UNIT ( * ) SI_UNIT ( .MILLI., .METRE. ) );
#68519=CARTESIAN_POINT ( 'NONE',  ( -32.58324634911704720, -8.999709270181572407, 4.695517540643423082 ) ) ;
#68524=VECTOR ( 'NONE', #62641, 1000.000000000000000 ) ;
#68530=ORIENTED_EDGE ( 'NONE', *, *, #7326, .F. ) ;
#68588=VERTEX_POINT ( 'NONE', #13943 ) ;
#68620=CARTESIAN_POINT ( 'NONE',  ( -55.16874038549254067, -8.628515624790349392, 6.699332285580846147 ) ) ;
#68623=ORIENTED_EDGE ( 'NONE', *, *, #24557, .F. ) ;
#68638=AXIS2_PLACEMENT_3D ( 'NONE', #49877, #44631, #64983 ) ;
#68653=CARTESIAN_POINT ( 'NONE',  ( -34.31243252642735087, -10.02680648607962510, -3.499999999999997335 ) ) ;
#68669=CARTESIAN_POINT ( 'NONE',  ( -58.54039790200148730, -8.499999999999465317, -0.1927383919051781080 ) ) ;
#68731=CARTESIAN_POINT ( 'NONE',  ( -11.99999999999999822, -8.499999999999998224, 3.000000000000000000 ) ) ;
#68734=EDGE_CURVE ( 'NONE', #21323, #17133, #59251, .T. ) ;
#68738=CIRCLE ( 'NONE', #39519, 1.000000000000000888 ) ;
#68758=AXIS2_PLACEMENT_3D ( 'NONE', #12800, #3238, #23706 ) ;
#68777=DIRECTION ( 'NONE',  ( -0.000000000000000000, -1.000000000000000000, -0.000000000000000000 ) ) ;
#68778=CARTESIAN_POINT ( 'NONE',  ( -33.89861118948982721, -9.947368421052626530, 2.722470280083843619 ) ) ;
#68841=ORIENTED_EDGE ( 'NONE', *, *, #43019, .F. ) ;
#68868=DIRECTION ( 'NONE',  ( 1.000000000000000000, 0.000000000000000000, 0.000000000000000000 ) ) ;
#68886=DIRECTION ( 'NONE',  ( -1.189524669241239115E-16, -1.000000000000000000, -0.000000000000000000 ) ) ;
#68897=DIRECTION ( 'NONE',  ( -1.000000000000000000, 0.000000000000000000, 0.000000000000000000 ) ) ;
#68923=CARTESIAN_POINT ( 'NONE',  ( -87.50000000000000000, -3.500000000000000000, 24.00000000000000000 ) ) ;
#68963=ORIENTED_EDGE ( 'NONE', *, *, #68381, .F. ) ;
#68986=CARTESIAN_POINT ( 'NONE',  ( -17.75000000000000355, -4.000000000000000000, 24.00000000000000000 ) ) ;
#69000=DIRECTION ( 'NONE',  ( 0.000000000000000000, 0.000000000000000000, 1.000000000000000000 ) ) ;
#69054=VERTEX_POINT ( 'NONE', #68731 ) ;
#69106=LINE ( 'NONE', #52925, #43772 ) ;
#69129=EDGE_CURVE ( 'NONE', #48775, #53539, #3327, .T. ) ;
#69184=ORIENTED_EDGE ( 'NONE', *, *, #53607, .F. ) ;
#69229=CARTESIAN_POINT ( 'NONE',  ( -10.74999999999999645, 4.336808689942018722E-16, 20.00000000000000000 ) ) ;
#69233=AXIS2_PLACEMENT_3D ( 'NONE', #16532, #37994, #59377 ) ;
#69239=VECTOR ( 'NONE', #24378, 1000.000000000000000 ) ;
#69243=DIRECTION ( 'NONE',  ( 0.000000000000000000, 1.000000000000000000, 0.000000000000000000 ) ) ;
#69273=LINE ( 'NONE', #47517, #14986 ) ;
#69361=VECTOR ( 'NONE', #31999, 1000.000000000000000 ) ;
#69380=DIRECTION ( 'NONE',  ( -1.189524669241239115E-16, -1.000000000000000000, -0.000000000000000000 ) ) ;
#69444=CARTESIAN_POINT ( 'NONE',  ( -32.02582413434465991, -8.774267863477543727, -1.283165077963180023 ) ) ;
#69451=CARTESIAN_POINT ( 'NONE',  ( -40.04190075645215785, -13.49999999999999822, 0.8979962945199000401 ) ) ;
#69453=LINE ( 'NONE', #32858, #65700 ) ;
#69454=CARTESIAN_POINT ( 'NONE',  ( -76.75000000000000000, 4.336808689942018722E-16, 20.00000000000000000 ) ) ;
#69461=DIRECTION ( 'NONE',  ( 0.000000000000000000, 1.000000000000000000, 0.000000000000000000 ) ) ;
#69478=DIRECTION ( 'NONE',  ( 0.000000000000000000, 0.000000000000000000, 1.000000000000000000 ) ) ;
#69483=LINE ( 'NONE', #11072, #31875 ) ;
#69503=CARTESIAN_POINT ( 'NONE',  ( -32.76851741822840580, -9.107254030101904263, -2.000000000000000000 ) ) ;
#69513=CARTESIAN_POINT ( 'NONE',  ( 3.851859888774471706E-31, -8.500000000000000000, 23.00000000000000000 ) ) ;
#69531=ADVANCED_FACE ( 'NONE', ( #11871 ), #29337, .T. ) ;
#69544=CARTESIAN_POINT ( 'NONE',  ( -32.33125961450744512, -8.628515624790757954, 6.699332285579864710 ) ) ;
#69569=CARTESIAN_POINT ( 'NONE',  ( -39.78460846725723599, -11.70376609979392946, 3.331841550777793870 ) ) ;
#69594=ORIENTED_EDGE ( 'NONE', *, *, #11274, .F. ) ;
#69683=EDGE_CURVE ( 'NONE', #14317, #22460, #6836, .T. ) ;
#69689=COLOUR_RGB ( '', 0.09019608, 0.27058824, 0.51372549) ;
ENDSEC;
END-ISO-10303-21;
